ISO-10303-21;
HEADER;
FILE_DESCRIPTION (('STEP AP203'),
    '1' );
FILE_NAME ('1602p_c_41.step',
    '2026-10-31T14:11:27',
    ( '' ),
    ( '' ),
    'SwSTEP 2.0',
    'SolidWorks 2024',
    '' );
FILE_SCHEMA (( 'AUTOMOTIVE_DESIGN' ));
ENDSEC;

DATA;
#23=LINE ( 'NONE', #23425, #95 ) ;
#51=ORIENTED_EDGE ( 'NONE', *, *, #216, .T. ) ;
#61=CARTESIAN_POINT ( 'NONE',  ( 112.5523895830310011, 2.765522746992190140, 1.033500000000031838 ) ) ;
#64=ADVANCED_FACE ( 'NONE', ( #15712 ), #3464, .F. ) ;
#79=CARTESIAN_POINT ( 'NONE',  ( 41.24356139695900225, 11.92996613406550033, 15.90000000000000036 ) ) ;
#86=EDGE_LOOP ( 'NONE', ( #14496, #4097, #19761, #7467 ) ) ;
#95=VECTOR ( 'NONE', #9188, 1000.000000000000227 ) ;
#96=EDGE_CURVE ( 'NONE', #14120, #3226, #13723, .T. ) ;
#104=VERTEX_POINT ( 'NONE', #3345 ) ;
#117=ADVANCED_FACE ( 'NONE', ( #23398 ), #23180, .F. ) ;
#123=CARTESIAN_POINT ( 'NONE',  ( 50.76434296088209663, 17.41090750189739822, 1.033500000000035390 ) ) ;
#131=VERTEX_POINT ( 'NONE', #18186 ) ;
#147=ORIENTED_EDGE ( 'NONE', *, *, #4410, .F. ) ;
#148=CARTESIAN_POINT ( 'NONE',  ( 118.5310588935630136, -6.697506338400800452, -20.00000000000000000 ) ) ;
#155=PLANE ( 'NONE',  #7113 ) ;
#157=PLANE ( 'NONE',  #11148 ) ;
#170=DIRECTION ( 'NONE',  ( 0.2306359803922080343, 0.9730401042858022320, 7.611545645951921999E-14 ) ) ;
#171=VERTEX_POINT ( 'NONE', #5590 ) ;
#179=CYLINDRICAL_SURFACE ( 'NONE', #16897, 2.066999999999999726 ) ;
#183=CARTESIAN_POINT ( 'NONE',  ( 114.1489752661110089, -25.18526831983100323, 3.399999999999999911 ) ) ;
#185=CARTESIAN_POINT ( 'NONE',  ( 118.6002496876800052, -6.405594307115129560, 18.89999999999999858 ) ) ;
#207=DIRECTION ( 'NONE',  ( -0.9730401042858022320, 0.2306359803922080343, 5.959266323858941219E-17 ) ) ;
#214=ORIENTED_EDGE ( 'NONE', *, *, #2972, .F. ) ;
#216=EDGE_CURVE ( 'NONE', #1911, #563, #20207, .T. ) ;
#222=ORIENTED_EDGE ( 'NONE', *, *, #1641, .T. ) ;
#227=VERTEX_POINT ( 'NONE', #5838 ) ;
#232=CARTESIAN_POINT ( 'NONE',  ( 37.40573311221180575, -6.139030851290243618, 13.00000000000000000 ) ) ;
#256=CARTESIAN_POINT ( 'NONE',  ( 117.0319250210129951, -13.02226701625849969, -15.90000000000000036 ) ) ;
#263=AXIS2_PLACEMENT_3D ( 'NONE', #10601, #1540, #1662 ) ;
#286=ORIENTED_EDGE ( 'NONE', *, *, #15419, .F. ) ;
#299=CARTESIAN_POINT ( 'NONE',  ( 44.19498725252769589, 23.44315552359092791, 13.00000000000000000 ) ) ;
#300=VERTEX_POINT ( 'NONE', #21746 ) ;
#301=CARTESIAN_POINT ( 'NONE',  ( 118.4388045014059969, -7.086722380115170417, -18.89999999999999858 ) ) ;
#303=DIRECTION ( 'NONE',  ( 0.8511275218278948618, 0.5249589903860170104, -5.212440122911309516E-17 ) ) ;
#309=ORIENTED_EDGE ( 'NONE', *, *, #22135, .T. ) ;
#312=DIRECTION ( 'NONE',  ( 7.664170260637049561E-16, 3.491853980616970288E-15, -1.000000000000000000 ) ) ;
#314=ORIENTED_EDGE ( 'NONE', *, *, #22865, .F. ) ;
#323=EDGE_CURVE ( 'NONE', #7718, #22958, #10828, .T. ) ;
#336=ORIENTED_EDGE ( 'NONE', *, *, #4633, .T. ) ;
#338=ORIENTED_EDGE ( 'NONE', *, *, #96, .T. ) ;
#358=CARTESIAN_POINT ( 'NONE',  ( 60.98218416654081864, 14.99311160239461316, -13.00000000000000000 ) ) ;
#382=DIRECTION ( 'NONE',  ( -0.9730401042858024541, 0.2306359803922080898, 5.959266323858942451E-17 ) ) ;
#386=AXIS2_PLACEMENT_3D ( 'NONE', #4433, #11703, #4784 ) ;
#387=DIRECTION ( 'NONE',  ( 2.199957270158029814E-13, -9.825194207785550278E-30, -1.000000000000000000 ) ) ;
#400=EDGE_CURVE ( 'NONE', #9648, #22197, #1272, .T. ) ;
#401=ORIENTED_EDGE ( 'NONE', *, *, #1811, .T. ) ;
#406=ORIENTED_EDGE ( 'NONE', *, *, #6819, .F. ) ;
#408=PLANE ( 'NONE',  #10336 ) ;
#412=EDGE_CURVE ( 'NONE', #11681, #1999, #22204, .T. ) ;
#415=DIRECTION ( 'NONE',  ( 1.000000000000000000, 0.000000000000000000, 0.000000000000000000 ) ) ;
#424=ORIENTED_EDGE ( 'NONE', *, *, #14769, .F. ) ;
#426=DIRECTION ( 'NONE',  ( -0.2306359803922085339, -0.9730401042858022320, 0.000000000000000000 ) ) ;
#429=ORIENTED_EDGE ( 'NONE', *, *, #21082, .T. ) ;
#456=CARTESIAN_POINT ( 'NONE',  ( 61.93563330948220624, 19.01565939351212009, -13.00000000000000000 ) ) ;
#462=AXIS2_PLACEMENT_3D ( 'NONE', #21262, #17608, #4890 ) ;
#463=EDGE_LOOP ( 'NONE', ( #7815, #9677, #22986, #7812 ) ) ;
#477=FACE_OUTER_BOUND ( 'NONE', #722, .T. ) ;
#487=AXIS2_PLACEMENT_3D ( 'NONE', #6092, #13572, #13346 ) ;
#496=EDGE_LOOP ( 'NONE', ( #15105, #1345 ) ) ;
#497=PLANE ( 'NONE',  #847 ) ;
#498=EDGE_CURVE ( 'NONE', #6410, #20342, #16990, .T. ) ;
#503=VERTEX_POINT ( 'NONE', #20025 ) ;
#504=ORIENTED_EDGE ( 'NONE', *, *, #16314, .F. ) ;
#511=CIRCLE ( 'NONE', #17976, 2.499999999999999112 ) ;
#537=LINE ( 'NONE', #4699, #2759 ) ;
#546=CARTESIAN_POINT ( 'NONE',  ( 113.2033677465029911, -29.17473274740290279, -3.099999999999920153 ) ) ;
#562=DIRECTION ( 'NONE',  ( 0.2306359803922080898, 0.9730401042858024541, -2.572202231434325988E-16 ) ) ;
#563=VERTEX_POINT ( 'NONE', #6998 ) ;
#568=AXIS2_PLACEMENT_3D ( 'NONE', #4257, #18774, #20648 ) ;
#570=CARTESIAN_POINT ( 'NONE',  ( 113.9239269372040013, -8.791386740117969723, 3.438967838479089450E-14 ) ) ;
#582=CARTESIAN_POINT ( 'NONE',  ( 113.4570673249340018, -28.10438863268850085, -3.399999999999949729 ) ) ;
#591=ORIENTED_EDGE ( 'NONE', *, *, #15449, .T. ) ;
#595=EDGE_CURVE ( 'NONE', #21743, #4396, #5423, .T. ) ;
#610=CIRCLE ( 'NONE', #16928, 2.066999999999999726 ) ;
#611=ORIENTED_EDGE ( 'NONE', *, *, #216, .F. ) ;
#619=EDGE_CURVE ( 'NONE', #14838, #21047, #1807, .T. ) ;
#626=EDGE_CURVE ( 'NONE', #15831, #13288, #12347, .T. ) ;
#632=DIRECTION ( 'NONE',  ( -1.085472681297010170E-15, -4.321163532573060300E-15, -1.000000000000000000 ) ) ;
#640=CARTESIAN_POINT ( 'NONE',  ( 118.6002496876800052, -6.405594307115060282, 15.90000000000000036 ) ) ;
#644=EDGE_CURVE ( 'NONE', #13133, #11391, #14330, .T. ) ;
#646=CIRCLE ( 'NONE', #9006, 2.499999999999999112 ) ;
#661=EDGE_LOOP ( 'NONE', ( #8314, #14025 ) ) ;
#675=EDGE_CURVE ( 'NONE', #16036, #9718, #15138, .T. ) ;
#676=ORIENTED_EDGE ( 'NONE', *, *, #8180, .T. ) ;
#684=EDGE_CURVE ( 'NONE', #2339, #15644, #6765, .T. ) ;
#689=ORIENTED_EDGE ( 'NONE', *, *, #9412, .F. ) ;
#700=EDGE_LOOP ( 'NONE', ( #22607, #4865 ) ) ;
#702=EDGE_LOOP ( 'NONE', ( #22974, #1504 ) ) ;
#720=DIRECTION ( 'NONE',  ( 5.810967191216043342E-28, 4.938475297218040001E-14, 1.000000000000000000 ) ) ;
#722=EDGE_LOOP ( 'NONE', ( #3744, #4350 ) ) ;
#729=DIRECTION ( 'NONE',  ( -0.9730401042858022320, 0.2306359803922080343, 8.445809534385342559E-31 ) ) ;
#738=EDGE_CURVE ( 'NONE', #12414, #131, #2184, .T. ) ;
#752=EDGE_CURVE ( 'NONE', #10345, #1222, #13375, .T. ) ;
#757=AXIS2_PLACEMENT_3D ( 'NONE', #19049, #10151, #729 ) ;
#770=ADVANCED_FACE ( 'NONE', ( #18377, #4353 ), #408, .T. ) ;
#771=DIRECTION ( 'NONE',  ( -0.9730401042858024541, 0.2306359803922080898, 5.959266323858942451E-17 ) ) ;
#781=ORIENTED_EDGE ( 'NONE', *, *, #11287, .F. ) ;
#794=DIRECTION ( 'NONE',  ( 1.426882515614939919E-15, 5.761552236122200693E-15, 1.000000000000000000 ) ) ;
#797=LINE ( 'NONE', #15303, #11528 ) ;
#813=VERTEX_POINT ( 'NONE', #7558 ) ;
#824=AXIS2_PLACEMENT_3D ( 'NONE', #5294, #21212, #10795 ) ;
#828=VECTOR ( 'NONE', #6564, 1000.000000000000227 ) ;
#833=EDGE_CURVE ( 'NONE', #21153, #11037, #11400, .T. ) ;
#839=VECTOR ( 'NONE', #16919, 1000.000000000000000 ) ;
#842=VECTOR ( 'NONE', #12317, 1000.000000000000000 ) ;
#846=ADVANCED_FACE ( 'NONE', ( #11729 ), #15615, .T. ) ;
#847=AXIS2_PLACEMENT_3D ( 'NONE', #20575, #20337, #11694 ) ;
#849=EDGE_LOOP ( 'NONE', ( #17166, #16409 ) ) ;
#858=CARTESIAN_POINT ( 'NONE',  ( 122.7747609327790030, 11.20643158045800014, -9.133960000000000079 ) ) ;
#867=DIRECTION ( 'NONE',  ( 0.2306359803922095053, 0.9730401042858018990, 0.000000000000000000 ) ) ;
#869=DIRECTION ( 'NONE',  ( -3.469446951953612296E-14, -1.908195823574486794E-13, -1.000000000000000000 ) ) ;
#880=AXIS2_PLACEMENT_3D ( 'NONE', #3587, #2349, #21614 ) ;
#882=AXIS2_PLACEMENT_3D ( 'NONE', #3490, #23429, #9309 ) ;
#883=ORIENTED_EDGE ( 'NONE', *, *, #14280, .F. ) ;
#884=DIRECTION ( 'NONE',  ( 0.2306359803922053697, 0.9730401042858028982, 0.000000000000000000 ) ) ;
#885=DIRECTION ( 'NONE',  ( -1.578894428126670167E-37, -2.578073951805180219E-21, 1.000000000000000000 ) ) ;
#889=CARTESIAN_POINT ( 'NONE',  ( 102.8131131701580046, 7.202356331284519797, 13.00000000000000000 ) ) ;
#892=EDGE_CURVE ( 'NONE', #2209, #19953, #2563, .T. ) ;
#902=CARTESIAN_POINT ( 'NONE',  ( 111.8137341348020044, 5.068973512656540059, -13.00000000000000000 ) ) ;
#911=VECTOR ( 'NONE', #21579, 1000.000000000000227 ) ;
#915=ORIENTED_EDGE ( 'NONE', *, *, #10858, .F. ) ;
#926=ADVANCED_FACE ( 'NONE', ( #995 ), #22736, .F. ) ;
#936=ORIENTED_EDGE ( 'NONE', *, *, #1650, .T. ) ;
#937=CARTESIAN_POINT ( 'NONE',  ( 55.46237324781409939, -8.294657213477510282, -13.00000000000000000 ) ) ;
#940=ORIENTED_EDGE ( 'NONE', *, *, #10661, .T. ) ;
#941=VECTOR ( 'NONE', #794, 1000.000000000000000 ) ;
#953=AXIS2_PLACEMENT_3D ( 'NONE', #11024, #12350, #3295 ) ;
#972=ADVANCED_FACE ( 'NONE', ( #1236 ), #9940, .T. ) ;
#973=CARTESIAN_POINT ( 'NONE',  ( 37.88245768368250310, -4.127756955731490152, -13.00000000000000000 ) ) ;
#975=AXIS2_PLACEMENT_3D ( 'NONE', #21938, #1876, #5674 ) ;
#976=ADVANCED_FACE ( 'NONE', ( #20840 ), #17168, .F. ) ;
#982=FACE_OUTER_BOUND ( 'NONE', #5351, .T. ) ;
#983=CARTESIAN_POINT ( 'NONE',  ( 114.9904400984929254, 13.05151942359561978, 2.500000000000071498 ) ) ;
#984=VECTOR ( 'NONE', #14388, 1000.000000000000227 ) ;
#990=VERTEX_POINT ( 'NONE', #3152 ) ;
#995=FACE_OUTER_BOUND ( 'NONE', #9985, .T. ) ;
#997=DIRECTION ( 'NONE',  ( -0.2306359803922085339, -0.9730401042858022320, 0.000000000000000000 ) ) ;
#999=VECTOR ( 'NONE', #4794, 1000.000000000000227 ) ;
#1000=CIRCLE ( 'NONE', #12790, 0.4000000000000010214 ) ;
#1005=VERTEX_POINT ( 'NONE', #17999 ) ;
#1006=CARTESIAN_POINT ( 'NONE',  ( 122.4288069621910040, 9.746871424029270869, 10.02499999999999858 ) ) ;
#1007=LINE ( 'NONE', #16940, #9510 ) ;
#1026=VECTOR ( 'NONE', #20309, 1000.000000000000227 ) ;
#1030=CONICAL_SURFACE ( 'NONE', #14324, 2.283500000000000085, 0.7853981633974469467 ) ;
#1038=EDGE_CURVE ( 'NONE', #14262, #8503, #5056, .T. ) ;
#1041=FACE_OUTER_BOUND ( 'NONE', #16334, .T. ) ;
#1046=ORIENTED_EDGE ( 'NONE', *, *, #17043, .T. ) ;
#1050=CONICAL_SURFACE ( 'NONE', #16592, 2.283500000000000085, 0.7853981633974469467 ) ;
#1051=ORIENTED_EDGE ( 'NONE', *, *, #20948, .T. ) ;
#1057=EDGE_CURVE ( 'NONE', #9718, #13613, #21310, .T. ) ;
#1059=PLANE ( 'NONE',  #3913 ) ;
#1063=VERTEX_POINT ( 'NONE', #17759 ) ;
#1068=CARTESIAN_POINT ( 'NONE',  ( 112.6956120935900003, 3.369770385951889935, 3.165715546043859906E-14 ) ) ;
#1070=CARTESIAN_POINT ( 'NONE',  ( 43.14167273007649328, 18.99928136731766770, 13.00000000000000000 ) ) ;
#1072=DIRECTION ( 'NONE',  ( -0.9730401042858024541, 0.2306359803922080898, 5.959266323853792669E-17 ) ) ;
#1078=CARTESIAN_POINT ( 'NONE',  ( 53.10252809683450437, 27.27557781334509812, 3.299332471243299474E-14 ) ) ;
#1080=ORIENTED_EDGE ( 'NONE', *, *, #8568, .T. ) ;
#1083=CARTESIAN_POINT ( 'NONE',  ( 113.9197686726213448, -24.27486053345101169, 13.00000000000000000 ) ) ;
#1106=CARTESIAN_POINT ( 'NONE',  ( 122.4288069621910040, 9.746871424029281528, -13.00000000000000000 ) ) ;
#1114=EDGE_CURVE ( 'NONE', #21559, #18063, #16209, .T. ) ;
#1116=DIRECTION ( 'NONE',  ( -3.469446951953612296E-14, -1.908195823574486794E-13, -1.000000000000000000 ) ) ;
#1132=AXIS2_PLACEMENT_3D ( 'NONE', #13582, #7283, #14395 ) ;
#1133=EDGE_CURVE ( 'NONE', #12333, #15644, #7534, .T. ) ;
#1136=CYLINDRICAL_SURFACE ( 'NONE', #4694, 0.4000000000000010214 ) ;
#1152=ORIENTED_EDGE ( 'NONE', *, *, #10914, .F. ) ;
#1165=EDGE_LOOP ( 'NONE', ( #3961, #781, #20696, #6323 ) ) ;
#1187=ORIENTED_EDGE ( 'NONE', *, *, #12685, .T. ) ;
#1197=ORIENTED_EDGE ( 'NONE', *, *, #21118, .F. ) ;
#1198=CARTESIAN_POINT ( 'NONE',  ( 117.0319250210129951, -13.02226701625859917, 15.90000000000000036 ) ) ;
#1203=CARTESIAN_POINT ( 'NONE',  ( 38.03772126950729415, -1.595291315507239682, -13.00000000000000000 ) ) ;
#1222=VERTEX_POINT ( 'NONE', #14653 ) ;
#1224=CARTESIAN_POINT ( 'NONE',  ( 118.4388045014059969, -7.086722380115130449, 18.89999999999999858 ) ) ;
#1236=FACE_OUTER_BOUND ( 'NONE', #21795, .T. ) ;
#1260=DIRECTION ( 'NONE',  ( -0.9730401042858022320, 0.2306359803922080343, 5.959266323858941219E-17 ) ) ;
#1268=LINE ( 'NONE', #7100, #8065 ) ;
#1272=LINE ( 'NONE', #19112, #3711 ) ;
#1280=EDGE_CURVE ( 'NONE', #21109, #18063, #11471, .T. ) ;
#1288=PLANE ( 'NONE',  #16185 ) ;
#1300=LINE ( 'NONE', #8565, #4668 ) ;
#1304=CARTESIAN_POINT ( 'NONE',  ( 118.5079952955230027, -6.794810348829399160, 15.50000000000000000 ) ) ;
#1308=DIRECTION ( 'NONE',  ( -0.9730401042858022320, 0.2306359803922080343, 5.959266323858941219E-17 ) ) ;
#1330=DIRECTION ( 'NONE',  ( 0.9730401042858024541, -0.2306359803922080898, -5.959266323858942451E-17 ) ) ;
#1342=ORIENTED_EDGE ( 'NONE', *, *, #12866, .F. ) ;
#1345=ORIENTED_EDGE ( 'NONE', *, *, #22589, .F. ) ;
#1347=LINE ( 'NONE', #5154, #18326 ) ;
#1350=ORIENTED_EDGE ( 'NONE', *, *, #21538, .F. ) ;
#1353=DIRECTION ( 'NONE',  ( -0.8511275218278966381, -0.5249589903860140128, 5.212440122911323074E-17 ) ) ;
#1356=PLANE ( 'NONE',  #13399 ) ;
#1360=ORIENTED_EDGE ( 'NONE', *, *, #12888, .T. ) ;
#1364=DIRECTION ( 'NONE',  ( -0.2306359803922053142, -0.9730401042858028982, 0.000000000000000000 ) ) ;
#1368=ORIENTED_EDGE ( 'NONE', *, *, #11010, .F. ) ;
#1380=VECTOR ( 'NONE', #15366, 1000.000000000000000 ) ;
#1385=EDGE_CURVE ( 'NONE', #15644, #2339, #5971, .T. ) ;
#1389=LINE ( 'NONE', #3298, #11151 ) ;
#1398=LINE ( 'NONE', #6883, #5855 ) ;
#1410=VECTOR ( 'NONE', #17002, 1000.000000000000227 ) ;
#1430=DIRECTION ( 'NONE',  ( 0.2306359803922053697, 0.9730401042858028982, 0.000000000000000000 ) ) ;
#1438=ADVANCED_FACE ( 'NONE', ( #2533 ), #2888, .T. ) ;
#1442=CARTESIAN_POINT ( 'NONE',  ( 41.24356139695900225, 11.92996613406550033, -15.90000000000000036 ) ) ;
#1443=LINE ( 'NONE', #15935, #15943 ) ;
#1447=DIRECTION ( 'NONE',  ( -0.1982893547227609354, -0.8365715274350927766, 0.5107146084542198983 ) ) ;
#1454=ORIENTED_EDGE ( 'NONE', *, *, #8240, .F. ) ;
#1455=DIRECTION ( 'NONE',  ( -0.9730401042858022320, 0.2306359803922080343, 5.959266323858941219E-17 ) ) ;
#1460=AXIS2_PLACEMENT_3D ( 'NONE', #5786, #20157, #10806 ) ;
#1468=CARTESIAN_POINT ( 'NONE',  ( 43.14167273007649328, 18.99928136731766770, -13.00000000000000000 ) ) ;
#1470=ADVANCED_FACE ( 'NONE', ( #13469 ), #20703, .T. ) ;
#1474=ORIENTED_EDGE ( 'NONE', *, *, #323, .F. ) ;
#1475=CARTESIAN_POINT ( 'NONE',  ( 113.4570673249340018, -28.10438863268850085, 3.399999999999999911 ) ) ;
#1480=AXIS2_PLACEMENT_3D ( 'NONE', #15233, #22343, #13342 ) ;
#1485=DIRECTION ( 'NONE',  ( 0.9730401042858024541, -0.2306359803922080898, -5.959266323858952312E-17 ) ) ;
#1500=DIRECTION ( 'NONE',  ( 0.000000000000000000, 0.000000000000000000, -1.000000000000000000 ) ) ;
#1504=ORIENTED_EDGE ( 'NONE', *, *, #2070, .F. ) ;
#1526=EDGE_CURVE ( 'NONE', #4592, #10583, #1443, .T. ) ;
#1540=DIRECTION ( 'NONE',  ( 0.1177891644214439926, 0.4969457958704997513, -0.8597503060258446794 ) ) ;
#1555=DIRECTION ( 'NONE',  ( -1.304396158928310329E-15, -5.761557392270100456E-15, 1.000000000000000000 ) ) ;
#1568=AXIS2_PLACEMENT_3D ( 'NONE', #19387, #12390, #17841 ) ;
#1580=VERTEX_POINT ( 'NONE', #6933 ) ;
#1590=DIRECTION ( 'NONE',  ( -0.9730401042858024541, 0.2306359803922080898, 5.959266323858942451E-17 ) ) ;
#1593=FACE_OUTER_BOUND ( 'NONE', #6313, .T. ) ;
#1603=VECTOR ( 'NONE', #18915, 1000.000000000000227 ) ;
#1632=VERTEX_POINT ( 'NONE', #21509 ) ;
#1641=EDGE_CURVE ( 'NONE', #16103, #3586, #12506, .T. ) ;
#1648=LINE ( 'NONE', #10236, #7807 ) ;
#1650=EDGE_CURVE ( 'NONE', #3196, #15865, #10501, .T. ) ;
#1653=( LENGTH_UNIT ( ) NAMED_UNIT ( * ) SI_UNIT ( .MILLI., .METRE. ) );
#1657=EDGE_CURVE ( 'NONE', #6574, #7703, #12395, .T. ) ;
#1658=ORIENTED_EDGE ( 'NONE', *, *, #19611, .T. ) ;
#1662=DIRECTION ( 'NONE',  ( -0.9907450477976873504, 0.000000000000000000, -0.1357359578901564667 ) ) ;
#1667=CARTESIAN_POINT ( 'NONE',  ( 46.46175228317039796, -6.161274394849590053, -13.00000000000000000 ) ) ;
#1671=ORIENTED_EDGE ( 'NONE', *, *, #4604, .F. ) ;
#1686=CARTESIAN_POINT ( 'NONE',  ( 118.6002496876800052, -6.405594307115129560, 18.89999999999999858 ) ) ;
#1696=EDGE_CURVE ( 'NONE', #1911, #2422, #14515, .T. ) ;
#1697=PRODUCT ( '1602p_c_41', '1602p_c_41', '', ( #2016 ) ) ;
#1699=CARTESIAN_POINT ( 'NONE',  ( 54.98564867634340203, -10.30593110903627441, -13.00000000000000000 ) ) ;
#1703=EDGE_CURVE ( 'NONE', #7758, #10964, #18189, .T. ) ;
#1707=VECTOR ( 'NONE', #2009, 1000.000000000000000 ) ;
#1711=ADVANCED_FACE ( 'NONE', ( #477 ), #5705, .F. ) ;
#1715=DIRECTION ( 'NONE',  ( -0.2306359803921919083, -0.9730401042858062288, -4.336808689942036669E-14 ) ) ;
#1730=EDGE_LOOP ( 'NONE', ( #5320, #15794 ) ) ;
#1759=VECTOR ( 'NONE', #19079, 1000.000000000000227 ) ;
#1768=DIRECTION ( 'NONE',  ( 0.8511275218278948618, 0.5249589903860170104, -5.212440122911309516E-17 ) ) ;
#1771=LINE ( 'NONE', #15810, #14181 ) ;
#1772=LINE ( 'NONE', #5576, #22850 ) ;
#1773=AXIS2_PLACEMENT_3D ( 'NONE', #2635, #16883, #7865 ) ;
#1776=DIRECTION ( 'NONE',  ( 0.2306359803922085339, 0.9730401042858022320, 0.000000000000000000 ) ) ;
#1781=VECTOR ( 'NONE', #21078, 1000.000000000000000 ) ;
#1788=FACE_OUTER_BOUND ( 'NONE', #12114, .T. ) ;
#1794=CARTESIAN_POINT ( 'NONE',  ( 118.5310588935630136, -6.697506338400800452, -20.00000000000000000 ) ) ;
#1807=CIRCLE ( 'NONE', #21522, 0.3999999999999998557 ) ;
#1811=EDGE_CURVE ( 'NONE', #3857, #7119, #20440, .T. ) ;
#1814=DIRECTION ( 'NONE',  ( 5.791496838535410422E-15, 2.469238035320170149E-14, -1.000000000000000000 ) ) ;
#1817=PLANE ( 'NONE',  #20611 ) ;
#1820=AXIS2_PLACEMENT_3D ( 'NONE', #21514, #10622, #7054 ) ;
#1822=CARTESIAN_POINT ( 'NONE',  ( 53.20239347634441884, 27.69690417850089759, -2.499999999999986233 ) ) ;
#1857=EDGE_CURVE ( 'NONE', #21726, #9676, #5540, .T. ) ;
#1871=ORIENTED_EDGE ( 'NONE', *, *, #1641, .F. ) ;
#1876=DIRECTION ( 'NONE',  ( 0.2306359803922080898, 0.9730401042858024541, -2.572202231434325988E-16 ) ) ;
#1879=CIRCLE ( 'NONE', #4929, 12.49999999999999467 ) ;
#1885=ORIENTED_EDGE ( 'NONE', *, *, #9372, .F. ) ;
#1895=DIRECTION ( 'NONE',  ( -0.9730401042858024541, 0.2306359803922080898, 5.959266323858942451E-17 ) ) ;
#1896=ORIENTED_EDGE ( 'NONE', *, *, #5171, .F. ) ;
#1901=CARTESIAN_POINT ( 'NONE',  ( 36.79228697538940196, -6.849707878650510118, -3.000000000000000000 ) ) ;
#1906=EDGE_CURVE ( 'NONE', #9182, #5106, #15792, .T. ) ;
#1911=VERTEX_POINT ( 'NONE', #19145 ) ;
#1921=PLANE ( 'NONE',  #19801 ) ;
#1923=ORIENTED_EDGE ( 'NONE', *, *, #8571, .F. ) ;
#1925=ORIENTED_EDGE ( 'NONE', *, *, #22676, .F. ) ;
#1929=ORIENTED_EDGE ( 'NONE', *, *, #17674, .T. ) ;
#1946=DIRECTION ( 'NONE',  ( -0.9730401042858024541, 0.2306359803922080898, 5.959266323858942451E-17 ) ) ;
#1950=CARTESIAN_POINT ( 'NONE',  ( 102.8131131701580046, 7.202356331284519797, 13.00000000000000000 ) ) ;
#1978=PRODUCT_DEFINITION ( 'UNKNOWN', '', #16680, #4712 ) ;
#1990=CIRCLE ( 'NONE', #6931, 2.499999999999998224 ) ;
#1993=CIRCLE ( 'NONE', #23234, 2.066999999999999726 ) ;
#1999=VERTEX_POINT ( 'NONE', #13661 ) ;
#2009=DIRECTION ( 'NONE',  ( 0.1630842657209384816, 0.6880432561069583786, -0.7071067811865453523 ) ) ;
#2015=AXIS2_PLACEMENT_3D ( 'NONE', #10570, #17437, #21462 ) ;
#2016=MECHANICAL_CONTEXT ( 'NONE', #5034, 'mechanical' ) ;
#2029=VERTEX_POINT ( 'NONE', #2970 ) ;
#2030=LINE ( 'NONE', #16157, #7584 ) ;
#2033=ORIENTED_EDGE ( 'NONE', *, *, #619, .T. ) ;
#2044=VERTEX_POINT ( 'NONE', #12257 ) ;
#2055=EDGE_LOOP ( 'NONE', ( #14801, #2410 ) ) ;
#2066=DIRECTION ( 'NONE',  ( -0.2306359803922080343, -0.9730401042858022320, 1.412237191019910313E-17 ) ) ;
#2070=EDGE_CURVE ( 'NONE', #12472, #22197, #18058, .T. ) ;
#2078=EDGE_LOOP ( 'NONE', ( #19476, #6876, #3014, #406 ) ) ;
#2134=EDGE_CURVE ( 'NONE', #9676, #5106, #1648, .T. ) ;
#2139=DIRECTION ( 'NONE',  ( -0.9730401042858022320, 0.2306359803922080343, 5.959266323858941219E-17 ) ) ;
#2149=ORIENTED_EDGE ( 'NONE', *, *, #12866, .T. ) ;
#2150=DIRECTION ( 'NONE',  ( -0.5249589903860224505, 0.8511275218278915311, 1.187479569643817911E-16 ) ) ;
#2164=FACE_BOUND ( 'NONE', #496, .T. ) ;
#2171=AXIS2_PLACEMENT_3D ( 'NONE', #14413, #19765, #12658 ) ;
#2173=CARTESIAN_POINT ( 'NONE',  ( 117.1933702072879981, -12.34113894325840022, -19.59999999999999787 ) ) ;
#2177=DIRECTION ( 'NONE',  ( -0.2306359803922066187, -0.9730401042858026761, 0.000000000000000000 ) ) ;
#2184=CIRCLE ( 'NONE', #17378, 6.999999999999998224 ) ;
#2185=DIRECTION ( 'NONE',  ( 0.9730401042858024541, -0.2306359803922080898, -5.959266323858942451E-17 ) ) ;
#2209=VERTEX_POINT ( 'NONE', #22058 ) ;
#2219=DIRECTION ( 'NONE',  ( -0.2306359803922080343, -0.9730401042858022320, 2.539064864905560527E-14 ) ) ;
#2226=ORIENTED_EDGE ( 'NONE', *, *, #15706, .T. ) ;
#2238=ORIENTED_EDGE ( 'NONE', *, *, #1906, .T. ) ;
#2245=VERTEX_POINT ( 'NONE', #13063 ) ;
#2250=ORIENTED_EDGE ( 'NONE', *, *, #16123, .F. ) ;
#2254=DIRECTION ( 'NONE',  ( -0.9730401042858022320, 0.2306359803922080343, 5.959266323858941219E-17 ) ) ;
#2263=AXIS2_PLACEMENT_3D ( 'NONE', #11968, #2802, #15498 ) ;
#2266=ADVANCED_FACE ( 'NONE', ( #12817 ), #18165, .T. ) ;
#2267=ORIENTED_EDGE ( 'NONE', *, *, #5288, .F. ) ;
#2277=VERTEX_POINT ( 'NONE', #3562 ) ;
#2278=DIRECTION ( 'NONE',  ( -0.9730401042858024541, 0.2306359803922080898, 5.959266323858942451E-17 ) ) ;
#2284=CARTESIAN_POINT ( 'NONE',  ( 49.94654008041209892, 6.372928970669730298, 3.830789599272820115E-14 ) ) ;
#2289=AXIS2_PLACEMENT_3D ( 'NONE', #23190, #15610, #19643 ) ;
#2290=FACE_OUTER_BOUND ( 'NONE', #17184, .T. ) ;
#2291=ADVANCED_FACE ( 'NONE', ( #11050 ), #13874, .F. ) ;
#2299=FACE_OUTER_BOUND ( 'NONE', #2078, .T. ) ;
#2314=VERTEX_POINT ( 'NONE', #10897 ) ;
#2322=CARTESIAN_POINT ( 'NONE',  ( 117.1011158151309957, -12.73035498497280038, -20.00000000000000000 ) ) ;
#2339=VERTEX_POINT ( 'NONE', #9206 ) ;
#2340=CARTESIAN_POINT ( 'NONE',  ( 60.58686099915964718, 8.989428683274725884, 3.765625566660095716E-14 ) ) ;
#2349=DIRECTION ( 'NONE',  ( -0.9730401042858024541, 0.2306359803922080898, 5.959266323854002210E-17 ) ) ;
#2356=DIRECTION ( 'NONE',  ( -0.9730401042858024541, 0.2306359803922080898, 5.959266323858942451E-17 ) ) ;
#2360=VECTOR ( 'NONE', #21663, 1000.000000000000114 ) ;
#2367=DIRECTION ( 'NONE',  ( -0.9730401042858022320, 0.2306359803922080343, 5.959266323858941219E-17 ) ) ;
#2369=ADVANCED_FACE ( 'NONE', ( #18009 ), #8578, .F. ) ;
#2379=VECTOR ( 'NONE', #3742, 1000.000000000000227 ) ;
#2384=ORIENTED_EDGE ( 'NONE', *, *, #738, .F. ) ;
#2389=EDGE_CURVE ( 'NONE', #8564, #22253, #7435, .T. ) ;
#2394=EDGE_CURVE ( 'NONE', #14881, #6574, #5522, .T. ) ;
#2407=EDGE_CURVE ( 'NONE', #22253, #8564, #18825, .T. ) ;
#2409=CARTESIAN_POINT ( 'NONE',  ( 113.4570673249340018, -28.10438863268850085, 3.399999999999999911 ) ) ;
#2410=ORIENTED_EDGE ( 'NONE', *, *, #12741, .T. ) ;
#2412=FACE_BOUND ( 'NONE', #4820, .T. ) ;
#2422=VERTEX_POINT ( 'NONE', #14427 ) ;
#2431=DIRECTION ( 'NONE',  ( -0.9730401042858024541, 0.2306359803922080898, 5.959266323858942451E-17 ) ) ;
#2444=FACE_OUTER_BOUND ( 'NONE', #4660, .T. ) ;
#2449=ORIENTED_EDGE ( 'NONE', *, *, #21301, .T. ) ;
#2452=ORIENTED_EDGE ( 'NONE', *, *, #10875, .T. ) ;
#2468=EDGE_LOOP ( 'NONE', ( #8073, #14635, #15259, #20781 ) ) ;
#2479=CARTESIAN_POINT ( 'NONE',  ( 50.90756547144189881, 18.01515514085709668, 3.544128957608909560E-14 ) ) ;
#2528=AXIS2_PLACEMENT_3D ( 'NONE', #22951, #3244, #15948 ) ;
#2532=DIRECTION ( 'NONE',  ( 6.124378941434239724E-17, -2.274246353359159970E-33, 1.000000000000000000 ) ) ;
#2533=FACE_OUTER_BOUND ( 'NONE', #11728, .T. ) ;
#2537=FACE_OUTER_BOUND ( 'NONE', #13025, .T. ) ;
#2541=AXIS2_PLACEMENT_3D ( 'NONE', #2566, #4466, #997 ) ;
#2554=ORIENTED_EDGE ( 'NONE', *, *, #6613, .T. ) ;
#2557=AXIS2_PLACEMENT_3D ( 'NONE', #7288, #23418, #3821 ) ;
#2562=CIRCLE ( 'NONE', #5585, 0.4000000000000010214 ) ;
#2563=LINE ( 'NONE', #10294, #3032 ) ;
#2566=CARTESIAN_POINT ( 'NONE',  ( 43.87899317387989839, 21.17128575569940097, -13.00000000000000000 ) ) ;
#2569=CARTESIAN_POINT ( 'NONE',  ( 0.000000000000000000, 0.000000000000000000, 0.000000000000000000 ) ) ;
#2582=LINE ( 'NONE', #13267, #22238 ) ;
#2586=DIRECTION ( 'NONE',  ( 1.524428182562999945E-15, 6.173091865707990781E-15, 1.000000000000000000 ) ) ;
#2588=VERTEX_POINT ( 'NONE', #13125 ) ;
#2595=EDGE_CURVE ( 'NONE', #15865, #13888, #5991, .T. ) ;
#2597=VECTOR ( 'NONE', #1447, 999.9999999999998863 ) ;
#2598=LINE ( 'NONE', #8062, #941 ) ;
#2609=VERTEX_POINT ( 'NONE', #16912 ) ;
#2617=ORIENTED_EDGE ( 'NONE', *, *, #17945, .T. ) ;
#2619=ORIENTED_EDGE ( 'NONE', *, *, #11412, .F. ) ;
#2621=LINE ( 'NONE', #13200, #9974 ) ;
#2635=CARTESIAN_POINT ( 'NONE',  ( 80.84056339148629888, -0.9497634067828859550, 3.641582893490300021E-14 ) ) ;
#2640=ADVANCED_FACE ( 'NONE', ( #5036 ), #15723, .T. ) ;
#2654=CARTESIAN_POINT ( 'NONE',  ( 41.15130700480209924, 11.54075009235119964, 15.90000000000000036 ) ) ;
#2664=ORIENTED_EDGE ( 'NONE', *, *, #5584, .F. ) ;
#2702=VECTOR ( 'NONE', #11036, 1000.000000000000000 ) ;
#2703=ORIENTED_EDGE ( 'NONE', *, *, #20444, .T. ) ;
#2704=ORIENTED_EDGE ( 'NONE', *, *, #19706, .F. ) ;
#2706=DIRECTION ( 'NONE',  ( -0.2306359803921919083, -0.9730401042858062288, 0.000000000000000000 ) ) ;
#2711=ADVANCED_FACE ( 'NONE', ( #17745 ), #19402, .F. ) ;
#2718=AXIS2_PLACEMENT_3D ( 'NONE', #7836, #15072, #13183 ) ;
#2719=VERTEX_POINT ( 'NONE', #983 ) ;
#2725=CARTESIAN_POINT ( 'NONE',  ( 118.4388045014059969, -7.086722380115130449, 18.89999999999999858 ) ) ;
#2727=EDGE_CURVE ( 'NONE', #9837, #21452, #9750, .T. ) ;
#2728=PLANE ( 'NONE',  #19279 ) ;
#2731=ORIENTED_EDGE ( 'NONE', *, *, #17971, .F. ) ;
#2743=EDGE_CURVE ( 'NONE', #7183, #21038, #21858, .T. ) ;
#2753=CARTESIAN_POINT ( 'NONE',  ( 118.5310588935630136, -6.697506338400819992, 20.00000000000000000 ) ) ;
#2756=ORIENTED_EDGE ( 'NONE', *, *, #20592, .F. ) ;
#2757=VECTOR ( 'NONE', #13947, 1000.000000000000227 ) ;
#2759=VECTOR ( 'NONE', #16812, 1000.000000000000000 ) ;
#2760=CARTESIAN_POINT ( 'NONE',  ( 118.6002496876800052, -6.405594307115080710, -18.89999999999999858 ) ) ;
#2766=ORIENTED_EDGE ( 'NONE', *, *, #6328, .T. ) ;
#2767=CARTESIAN_POINT ( 'NONE',  ( 114.8905747189831033, 12.63019305843987539, 2.067000000000084103 ) ) ;
#2796=ORIENTED_EDGE ( 'NONE', *, *, #675, .T. ) ;
#2802=DIRECTION ( 'NONE',  ( -0.9730401042858023430, 0.2306359803922080620, 5.959266323858944916E-17 ) ) ;
#2811=EDGE_CURVE ( 'NONE', #13288, #1580, #21296, .T. ) ;
#2812=LINE ( 'NONE', #22619, #22671 ) ;
#2819=DIRECTION ( 'NONE',  ( -0.9730401042858024541, 0.2306359803922080898, 5.959266323853532591E-17 ) ) ;
#2853=DIRECTION ( 'NONE',  ( 0.2306359803922085339, 0.9730401042858022320, 0.000000000000000000 ) ) ;
#2881=ORIENTED_EDGE ( 'NONE', *, *, #6692, .T. ) ;
#2888=PLANE ( 'NONE',  #757 ) ;
#2898=DIRECTION ( 'NONE',  ( -0.9730401042858024541, 0.2306359803922080898, 5.959266323858942451E-17 ) ) ;
#2904=ORIENTED_EDGE ( 'NONE', *, *, #18858, .T. ) ;
#2908=VERTEX_POINT ( 'NONE', #3478 ) ;
#2925=LINE ( 'NONE', #8739, #21147 ) ;
#2926=FACE_OUTER_BOUND ( 'NONE', #19641, .T. ) ;
#2933=CIRCLE ( 'NONE', #22648, 0.3999999999999982458 ) ;
#2934=ORIENTED_EDGE ( 'NONE', *, *, #1385, .F. ) ;
#2943=CIRCLE ( 'NONE', #10938, 0.4000000000000010214 ) ;
#2953=CARTESIAN_POINT ( 'NONE',  ( 117.1011158151309957, -12.73035498497280038, 19.59999999999999787 ) ) ;
#2965=EDGE_LOOP ( 'NONE', ( #14831, #5186, #9095, #15766 ) ) ;
#2970=CARTESIAN_POINT ( 'NONE',  ( 41.17437060284130013, 11.63805410277980101, -20.00000000000000000 ) ) ;
#2972=EDGE_CURVE ( 'NONE', #19234, #9837, #11896, .T. ) ;
#2973=LINE ( 'NONE', #8322, #6788 ) ;
#2979=CARTESIAN_POINT ( 'NONE',  ( 39.74442752440959481, 5.605205456207779768, -20.00000000000000000 ) ) ;
#2984=ORIENTED_EDGE ( 'NONE', *, *, #8508, .F. ) ;
#2987=ADVANCED_FACE ( 'NONE', ( #10103 ), #16522, .T. ) ;
#2991=LINE ( 'NONE', #17484, #7349 ) ;
#3014=ORIENTED_EDGE ( 'NONE', *, *, #17997, .F. ) ;
#3020=PLANE ( 'NONE',  #13390 ) ;
#3021=EDGE_CURVE ( 'NONE', #21452, #9837, #19594, .T. ) ;
#3027=ADVANCED_FACE ( 'NONE', ( #18886 ), #20223, .T. ) ;
#3029=DIRECTION ( 'NONE',  ( 1.000000000000000000, 1.304396158928280155E-15, 0.000000000000000000 ) ) ;
#3032=VECTOR ( 'NONE', #9818, 1000.000000000000227 ) ;
#3034=CARTESIAN_POINT ( 'NONE',  ( 120.2377651484647032, 0.5029904333151811180, 13.00000000000000000 ) ) ;
#3048=VERTEX_POINT ( 'NONE', #20654 ) ;
#3083=ORIENTED_EDGE ( 'NONE', *, *, #2407, .T. ) ;
#3084=CARTESIAN_POINT ( 'NONE',  ( 35.84667945578129888, -10.83917230622230043, -13.00000000000000000 ) ) ;
#3096=ORIENTED_EDGE ( 'NONE', *, *, #19547, .F. ) ;
#3103=ORIENTED_EDGE ( 'NONE', *, *, #22094, .T. ) ;
#3129=DIRECTION ( 'NONE',  ( -0.9730401042858022320, 0.2306359803922080343, 1.587386801403055476E-31 ) ) ;
#3135=CARTESIAN_POINT ( 'NONE',  ( 36.10037903421270755, -9.768828191507889613, -3.399999999999939959 ) ) ;
#3152=CARTESIAN_POINT ( 'NONE',  ( 39.67523673029189979, 5.313293424921970320, 15.90000000000000036 ) ) ;
#3157=VECTOR ( 'NONE', #9745, 1000.000000000000000 ) ;
#3160=EDGE_CURVE ( 'NONE', #17030, #17831, #19985, .T. ) ;
#3166=VECTOR ( 'NONE', #14996, 1000.000000000000227 ) ;
#3172=ADVANCED_FACE ( 'NONE', ( #8901 ), #11674, .F. ) ;
#3173=ORIENTED_EDGE ( 'NONE', *, *, #5711, .F. ) ;
#3182=ORIENTED_EDGE ( 'NONE', *, *, #12741, .F. ) ;
#3187=CARTESIAN_POINT ( 'NONE',  ( 120.8143550994449953, 2.935590694028619829, -13.00000000000000000 ) ) ;
#3192=ORIENTED_EDGE ( 'NONE', *, *, #21762, .F. ) ;
#3194=DIRECTION ( 'NONE',  ( -0.2306359803922085339, -0.9730401042858022320, 0.000000000000000000 ) ) ;
#3196=VERTEX_POINT ( 'NONE', #19811 ) ;
#3197=ADVANCED_FACE ( 'NONE', ( #16126 ), #1288, .T. ) ;
#3226=VERTEX_POINT ( 'NONE', #17689 ) ;
#3235=AXIS2_PLACEMENT_3D ( 'NONE', #13284, #7587, #13065 ) ;
#3244=DIRECTION ( 'NONE',  ( -0.9730401042858024541, 0.2306359803922080898, 5.959266323858942451E-17 ) ) ;
#3265=CARTESIAN_POINT ( 'NONE',  ( 118.5079952955230027, -6.794810348829390279, 15.90000000000000036 ) ) ;
#3273=CARTESIAN_POINT ( 'NONE',  ( 37.46113131852679601, -4.027891576221660053, -20.00000000000000000 ) ) ;
#3275=DIRECTION ( 'NONE',  ( -0.9730401042858024541, 0.2306359803922080898, 5.959266323858942451E-17 ) ) ;
#3279=EDGE_LOOP ( 'NONE', ( #5422, #11798, #5153, #21974 ) ) ;
#3282=ORIENTED_EDGE ( 'NONE', *, *, #3425, .T. ) ;
#3295=DIRECTION ( 'NONE',  ( -1.982541115402064913E-15, -6.814985084194598285E-15, 1.000000000000000000 ) ) ;
#3298=CARTESIAN_POINT ( 'NONE',  ( 120.8143550994449953, 2.935590694028629599, 20.00000000000000000 ) ) ;
#3300=VECTOR ( 'NONE', #18970, 1000.000000000000227 ) ;
#3301=VECTOR ( 'NONE', #19518, 1000.000000000000227 ) ;
#3306=DIRECTION ( 'NONE',  ( -4.758660364968300250E-15, -2.033490192229560220E-14, 1.000000000000000000 ) ) ;
#3328=VERTEX_POINT ( 'NONE', #16696 ) ;
#3330=DIRECTION ( 'NONE',  ( -0.9730401042858024541, 0.2306359803922080898, 5.959266323858942451E-17 ) ) ;
#3345=CARTESIAN_POINT ( 'NONE',  ( 114.1489752661110089, -25.18526831983100323, -3.400000000000049649 ) ) ;
#3349=DIRECTION ( 'NONE',  ( -0.9730401042858022320, 0.2306359803922080343, 5.959266323858941219E-17 ) ) ;
#3356=DIRECTION ( 'NONE',  ( 0.000000000000000000, 0.000000000000000000, -1.000000000000000000 ) ) ;
#3369=CARTESIAN_POINT ( 'NONE',  ( 113.2956221386590130, -28.78551670568849730, 2.700000000000000178 ) ) ;
#3376=CARTESIAN_POINT ( 'NONE',  ( 43.66832999130209458, 21.22121844545429781, -13.00000000000000000 ) ) ;
#3382=CARTESIAN_POINT ( 'NONE',  ( 53.20239347634440463, 27.69690417850090114, 3.288194835581189691E-14 ) ) ;
#3384=CYLINDRICAL_SURFACE ( 'NONE', #6487, 2.066999999999998394 ) ;
#3406=AXIS2_PLACEMENT_3D ( 'NONE', #937, #12246, #2853 ) ;
#3410=EDGE_CURVE ( 'NONE', #20573, #1580, #14810, .T. ) ;
#3414=ORIENTED_EDGE ( 'NONE', *, *, #21285, .T. ) ;
#3425=EDGE_CURVE ( 'NONE', #9613, #21153, #3761, .T. ) ;
#3436=SHAPE_REPRESENTATION_RELATIONSHIP ( 'NONE' , 'NONE' ,  #20540, #14745 ) ;
#3460=ORIENTED_EDGE ( 'NONE', *, *, #23001, .F. ) ;
#3464=CYLINDRICAL_SURFACE ( 'NONE', #22045, 2.066999999999999726 ) ;
#3471=LINE ( 'NONE', #19744, #2597 ) ;
#3478=CARTESIAN_POINT ( 'NONE',  ( 38.03772126950729415, -1.595291315507239682, 13.00000000000000000 ) ) ;
#3483=DIRECTION ( 'NONE',  ( -0.9730401042858024541, 0.2306359803922080898, 5.959266323858932590E-17 ) ) ;
#3490=CARTESIAN_POINT ( 'NONE',  ( 115.8700071457750056, -9.252658700902388844, 3.427049305831379237E-14 ) ) ;
#3504=AXIS2_PLACEMENT_3D ( 'NONE', #13104, #720, #14987 ) ;
#3505=CARTESIAN_POINT ( 'NONE',  ( 55.93909781928478253, -6.283383317918767474, -13.00000000000000000 ) ) ;
#3509=DIRECTION ( 'NONE',  ( -0.2306359803922066187, -0.9730401042858026761, 0.000000000000000000 ) ) ;
#3512=ORIENTED_EDGE ( 'NONE', *, *, #1657, .T. ) ;
#3526=AXIS2_PLACEMENT_3D ( 'NONE', #3265, #17414, #6729 ) ;
#3537=DIRECTION ( 'NONE',  ( -0.2306359803922080343, -0.9730401042858022320, -5.907067092757111157E-15 ) ) ;
#3542=ORIENTED_EDGE ( 'NONE', *, *, #22589, .T. ) ;
#3554=ORIENTED_EDGE ( 'NONE', *, *, #14245, .T. ) ;
#3562=CARTESIAN_POINT ( 'NONE',  ( 96.33985310849000427, -20.10796027570521716, 13.00000000000000000 ) ) ;
#3564=FACE_OUTER_BOUND ( 'NONE', #15188, .T. ) ;
#3569=VECTOR ( 'NONE', #7839, 1000.000000000000227 ) ;
#3577=CARTESIAN_POINT ( 'NONE',  ( 96.81657767996070163, -18.09668638014640152, -13.00000000000000000 ) ) ;
#3583=ORIENTED_EDGE ( 'NONE', *, *, #19736, .T. ) ;
#3585=EDGE_LOOP ( 'NONE', ( #7907, #8312, #20226, #6658 ) ) ;
#3586=VERTEX_POINT ( 'NONE', #18862 ) ;
#3587=CARTESIAN_POINT ( 'NONE',  ( 36.79228697538940196, -6.849707878650520776, 3.000000000000000000 ) ) ;
#3591=LINE ( 'NONE', #14512, #21856 ) ;
#3594=EDGE_CURVE ( 'NONE', #19697, #2044, #17057, .T. ) ;
#3596=CARTESIAN_POINT ( 'NONE',  ( 44.19498725252769589, 23.44315552359092791, -13.00000000000000000 ) ) ;
#3607=ORIENTED_EDGE ( 'NONE', *, *, #2070, .T. ) ;
#3620=CARTESIAN_POINT ( 'NONE',  ( 118.5310588935630136, -6.697506338400810222, 19.59999999999999787 ) ) ;
#3631=AXIS2_PLACEMENT_3D ( 'NONE', #14557, #18118, #5633 ) ;
#3637=FACE_OUTER_BOUND ( 'NONE', #13224, .T. ) ;
#3651=CARTESIAN_POINT ( 'NONE',  ( 117.0319250210129951, -13.02226701625859917, 18.89999999999999858 ) ) ;
#3678=FACE_OUTER_BOUND ( 'NONE', #20537, .T. ) ;
#3688=ORIENTED_EDGE ( 'NONE', *, *, #8699, .F. ) ;
#3697=DIRECTION ( 'NONE',  ( -0.9730401042858023430, 0.2306359803922080620, 5.959266323858944916E-17 ) ) ;
#3698=VECTOR ( 'NONE', #9036, 1000.000000000000227 ) ;
#3701=DIRECTION ( 'NONE',  ( -0.5249589903860224505, 0.8511275218278915311, 1.187479569643817911E-16 ) ) ;
#3708=DIRECTION ( 'NONE',  ( 0.2306359803922076457, 0.9730401042858025651, -1.412237191019970710E-17 ) ) ;
#3711=VECTOR ( 'NONE', #17321, 1000.000000000000227 ) ;
#3719=ORIENTED_EDGE ( 'NONE', *, *, #2743, .F. ) ;
#3740=EDGE_CURVE ( 'NONE', #3048, #1063, #11442, .T. ) ;
#3742=DIRECTION ( 'NONE',  ( -0.9730401042858022320, 0.2306359803922080343, 5.959266323858941219E-17 ) ) ;
#3744=ORIENTED_EDGE ( 'NONE', *, *, #3021, .F. ) ;
#3745=EDGE_CURVE ( 'NONE', #23097, #21187, #6627, .T. ) ;
#3746=DIRECTION ( 'NONE',  ( 0.2306359803922095053, 0.9730401042858018990, 0.000000000000000000 ) ) ;
#3761=LINE ( 'NONE', #14694, #2702 ) ;
#3785=FACE_OUTER_BOUND ( 'NONE', #13387, .T. ) ;
#3786=LINE ( 'NONE', #9504, #22901 ) ;
#3790=CARTESIAN_POINT ( 'NONE',  ( 117.0319250210129951, -13.02226701625849969, -15.90000000000000036 ) ) ;
#3791=ORIENTED_EDGE ( 'NONE', *, *, #4675, .F. ) ;
#3792=AXIS2_PLACEMENT_3D ( 'NONE', #10274, #11825, #17500 ) ;
#3807=AXIS2_PLACEMENT_3D ( 'NONE', #902, #17307, #15042 ) ;
#3818=EDGE_CURVE ( 'NONE', #8021, #5959, #13017, .T. ) ;
#3821=DIRECTION ( 'NONE',  ( 0.000000000000000000, 0.000000000000000000, -1.000000000000000000 ) ) ;
#3822=CARTESIAN_POINT ( 'NONE',  ( 117.1011158151309957, -12.73035498497280038, -20.00000000000000000 ) ) ;
#3824=ORIENTED_EDGE ( 'NONE', *, *, #412, .T. ) ;
#3825=CARTESIAN_POINT ( 'NONE',  ( 113.4570673249340018, -28.10438863268850085, 3.399999999999999911 ) ) ;
#3832=ORIENTED_EDGE ( 'NONE', *, *, #12843, .F. ) ;
#3848=DIRECTION ( 'NONE',  ( -0.9730401042858024541, 0.2306359803922080898, 5.959266323858592394E-17 ) ) ;
#3857=VERTEX_POINT ( 'NONE', #10790 ) ;
#3863=VECTOR ( 'NONE', #13706, 1000.000000000000000 ) ;
#3872=CIRCLE ( 'NONE', #14876, 2.999999999999999556 ) ;
#3904=ADVANCED_FACE ( 'NONE', ( #9446 ), #22064, .F. ) ;
#3913=AXIS2_PLACEMENT_3D ( 'NONE', #5744, #3969, #387 ) ;
#3937=VECTOR ( 'NONE', #20155, 1000.000000000000114 ) ;
#3938=CARTESIAN_POINT ( 'NONE',  ( 50.76434296088209663, 17.41090750189739822, -1.033499999999964336 ) ) ;
#3943=DIRECTION ( 'NONE',  ( -0.9730401042858022320, 0.2306359803922080343, 5.959266323858941219E-17 ) ) ;
#3947=CARTESIAN_POINT ( 'NONE',  ( 61.45890873801150178, 17.00438549795339682, 13.00000000000000000 ) ) ;
#3950=CARTESIAN_POINT ( 'NONE',  ( 111.3370095633313070, 3.057699617097837219, 13.00000000000000000 ) ) ;
#3952=VERTEX_POINT ( 'NONE', #16915 ) ;
#3954=DIRECTION ( 'NONE',  ( -0.2306359803922053697, -0.9730401042858028982, 0.000000000000000000 ) ) ;
#3961=ORIENTED_EDGE ( 'NONE', *, *, #11411, .F. ) ;
#3964=DIRECTION ( 'NONE',  ( -0.9730401042858022320, 0.2306359803922080343, 5.959266323858941219E-17 ) ) ;
#3969=DIRECTION ( 'NONE',  ( 0.2306359803922080620, 0.9730401042858023430, 5.073893018238627926E-14 ) ) ;
#3987=EDGE_LOOP ( 'NONE', ( #9039, #12941 ) ) ;
#4004=ORIENTED_EDGE ( 'NONE', *, *, #6613, .F. ) ;
#4022=ADVANCED_FACE ( 'NONE', ( #2444 ), #6348, .F. ) ;
#4030=CARTESIAN_POINT ( 'NONE',  ( 111.3370095633313070, 3.057699617097787037, -13.00000000000000000 ) ) ;
#4038=DIRECTION ( 'NONE',  ( -0.9730401042858022320, 0.2306359803922080343, 5.959266323858951079E-17 ) ) ;
#4049=CONICAL_SURFACE ( 'NONE', #17328, 2.283499999999998753, 0.7853981633974433940 ) ;
#4058=VECTOR ( 'NONE', #17856, 1000.000000000000227 ) ;
#4070=ORIENTED_EDGE ( 'NONE', *, *, #16465, .F. ) ;
#4077=DIRECTION ( 'NONE',  ( -0.9730401042858022320, 0.2306359803922080343, -1.978423856035325353E-31 ) ) ;
#4079=CIRCLE ( 'NONE', #17361, 2.499999999999999112 ) ;
#4083=AXIS2_PLACEMENT_3D ( 'NONE', #9795, #8352, #21056 ) ;
#4089=DIRECTION ( 'NONE',  ( -0.9730401042858024541, 0.2306359803922080898, 5.959266323853292235E-17 ) ) ;
#4097=ORIENTED_EDGE ( 'NONE', *, *, #6692, .F. ) ;
#4104=CYLINDRICAL_SURFACE ( 'NONE', #12272, 7.000000000000000888 ) ;
#4111=ORIENTED_EDGE ( 'NONE', *, *, #7073, .T. ) ;
#4114=LINE ( 'NONE', #14930, #9248 ) ;
#4153=EDGE_LOOP ( 'NONE', ( #3182, #401, #18884, #12847 ) ) ;
#4166=CARTESIAN_POINT ( 'NONE',  ( 113.2033677465029911, -29.17473274740279976, 13.00000000000000000 ) ) ;
#4175=CARTESIAN_POINT ( 'NONE',  ( 58.28050119523756933, -0.7409723595832931053, 3.718515598612927419E-14 ) ) ;
#4217=EDGE_LOOP ( 'NONE', ( #21612, #14236, #4920, #17701 ) ) ;
#4244=CARTESIAN_POINT ( 'NONE',  ( 53.10252809683457542, 27.27557781334508036, 2.066999999999991733 ) ) ;
#4257=CARTESIAN_POINT ( 'NONE',  ( 80.84056339148629888, -0.9497634067828859550, 3.641582893490300021E-14 ) ) ;
#4258=AXIS2_PLACEMENT_3D ( 'NONE', #18151, #5546, #426 ) ;
#4262=EDGE_CURVE ( 'NONE', #2609, #10848, #12308, .T. ) ;
#4267=CARTESIAN_POINT ( 'NONE',  ( 49.94654008041209892, 6.372928970669730298, 3.830789599272820115E-14 ) ) ;
#4277=CARTESIAN_POINT ( 'NONE',  ( 113.2956221386590130, -28.78551670568859677, -2.700000000000000178 ) ) ;
#4278=DIRECTION ( 'NONE',  ( 0.2306359803922085339, 0.9730401042858022320, 0.000000000000000000 ) ) ;
#4311=EDGE_LOOP ( 'NONE', ( #7847, #4004, #9289, #17638 ) ) ;
#4333=ADVANCED_FACE ( 'NONE', ( #17990 ), #12646, .F. ) ;
#4335=DIRECTION ( 'NONE',  ( 6.124378941434239724E-17, -2.274246353359159970E-33, 1.000000000000000000 ) ) ;
#4341=CARTESIAN_POINT ( 'NONE',  ( 113.2956221386590130, -28.78551670568859677, -2.700000000000000178 ) ) ;
#4346=ADVANCED_FACE ( 'NONE', ( #21984 ), #14755, .T. ) ;
#4348=CARTESIAN_POINT ( 'NONE',  ( 41.24356139695900225, 11.92996613406550033, 15.90000000000000036 ) ) ;
#4350=ORIENTED_EDGE ( 'NONE', *, *, #2727, .F. ) ;
#4352=ORIENTED_EDGE ( 'NONE', *, *, #18811, .T. ) ;
#4353=FACE_OUTER_BOUND ( 'NONE', #18791, .T. ) ;
#4360=DIRECTION ( 'NONE',  ( -1.734723475976802677E-14, -4.336808689942006376E-14, -1.000000000000000000 ) ) ;
#4377=ORIENTED_EDGE ( 'NONE', *, *, #3021, .T. ) ;
#4387=ORIENTED_EDGE ( 'NONE', *, *, #19285, .T. ) ;
#4393=DIRECTION ( 'NONE',  ( -0.9730401042858024541, 0.2306359803922080898, 5.959266323858942451E-17 ) ) ;
#4395=EDGE_LOOP ( 'NONE', ( #8277, #51, #14788 ) ) ;
#4396=VERTEX_POINT ( 'NONE', #10759 ) ;
#4401=VERTEX_POINT ( 'NONE', #3825 ) ;
#4410=EDGE_CURVE ( 'NONE', #11739, #14649, #8954, .T. ) ;
#4414=DIRECTION ( 'NONE',  ( -0.2306359803921919083, -0.9730401042858062288, -1.333568672157176260E-13 ) ) ;
#4417=CARTESIAN_POINT ( 'NONE',  ( 44.35571774535060996, 23.18255965125822371, 13.00000000000000000 ) ) ;
#4419=ORIENTED_EDGE ( 'NONE', *, *, #19847, .T. ) ;
#4420=FACE_OUTER_BOUND ( 'NONE', #22781, .T. ) ;
#4432=CARTESIAN_POINT ( 'NONE',  ( 46.46175228317039796, -6.161274394849590053, 13.00000000000000000 ) ) ;
#4433=CARTESIAN_POINT ( 'NONE',  ( 118.4388045014059969, -7.086722380115130449, 19.59999999999999787 ) ) ;
#4436=CIRCLE ( 'NONE', #14670, 4.999999999999998224 ) ;
#4441=VECTOR ( 'NONE', #10978, 1000.000000000000227 ) ;
#4450=ADVANCED_FACE ( 'NONE', ( #20687 ), #11872, .F. ) ;
#4451=ADVANCED_FACE ( 'NONE', ( #2412, #2164, #13457, #4420, #6214, #22573 ), #497, .F. ) ;
#4463=DIRECTION ( 'NONE',  ( 0.9730401042858024541, -0.2306359803922080898, -5.959266323854002210E-17 ) ) ;
#4466=DIRECTION ( 'NONE',  ( 0.9730401042858024541, -0.2306359803922080898, -5.959266323858942451E-17 ) ) ;
#4471=LINE ( 'NONE', #546, #20623 ) ;
#4474=VECTOR ( 'NONE', #632, 1000.000000000000000 ) ;
#4487=ORIENTED_EDGE ( 'NONE', *, *, #12235, .T. ) ;
#4492=AXIS2_PLACEMENT_3D ( 'NONE', #6942, #5141, #5369 ) ;
#4506=VERTEX_POINT ( 'NONE', #22466 ) ;
#4509=ORIENTED_EDGE ( 'NONE', *, *, #18798, .T. ) ;
#4516=EDGE_CURVE ( 'NONE', #7758, #7718, #17125, .T. ) ;
#4528=DIRECTION ( 'NONE',  ( 0.000000000000000000, 4.336808689942006376E-14, 1.000000000000000000 ) ) ;
#4531=DIRECTION ( 'NONE',  ( -0.2306359803922076457, -0.9730401042858025651, 0.000000000000000000 ) ) ;
#4539=ADVANCED_FACE ( 'NONE', ( #18570 ), #8118, .F. ) ;
#4541=ADVANCED_FACE ( 'NONE', ( #9423 ), #9542, .F. ) ;
#4550=ADVANCED_FACE ( 'NONE', ( #5856 ), #16886, .T. ) ;
#4560=VECTOR ( 'NONE', #170, 1000.000000000000227 ) ;
#4573=DIRECTION ( 'NONE',  ( -0.9730401042858022320, 0.2306359803922080343, 5.959266323858941219E-17 ) ) ;
#4584=DIRECTION ( 'NONE',  ( -1.426882515614939919E-15, -5.761552236122200693E-15, -1.000000000000000000 ) ) ;
#4586=ADVANCED_FACE ( 'NONE', ( #17722 ), #19035, .T. ) ;
#4590=CIRCLE ( 'NONE', #17866, 7.000000000000000888 ) ;
#4592=VERTEX_POINT ( 'NONE', #6685 ) ;
#4594=CARTESIAN_POINT ( 'NONE',  ( 118.5310588935630136, -6.697506338400830650, -19.59999999999999787 ) ) ;
#4604=EDGE_CURVE ( 'NONE', #227, #19697, #3872, .T. ) ;
#4617=ORIENTED_EDGE ( 'NONE', *, *, #10219, .T. ) ;
#4620=EDGE_LOOP ( 'NONE', ( #3414, #17551, #14019, #1046 ) ) ;
#4623=DIRECTION ( 'NONE',  ( -0.9730401042858024541, 0.2306359803922080898, 5.959266323858942451E-17 ) ) ;
#4633=EDGE_CURVE ( 'NONE', #21933, #21767, #17475, .T. ) ;
#4643=AXIS2_PLACEMENT_3D ( 'NONE', #12040, #1072, #22810 ) ;
#4651=CARTESIAN_POINT ( 'NONE',  ( 112.2904587062726876, 7.080247408215343263, 13.00000000000000000 ) ) ;
#4652=VECTOR ( 'NONE', #20572, 1000.000000000000227 ) ;
#4654=ORIENTED_EDGE ( 'NONE', *, *, #12971, .F. ) ;
#4659=LINE ( 'NONE', #2760, #7303 ) ;
#4660=EDGE_LOOP ( 'NONE', ( #18032, #19608, #16229, #4387 ) ) ;
#4664=ORIENTED_EDGE ( 'NONE', *, *, #10718, .F. ) ;
#4668=VECTOR ( 'NONE', #15795, 1000.000000000000227 ) ;
#4675=EDGE_CURVE ( 'NONE', #14157, #16389, #16768, .T. ) ;
#4679=CARTESIAN_POINT ( 'NONE',  ( 52.05497947389309843, 22.85602965967900246, 2.067000000000033921 ) ) ;
#4685=CARTESIAN_POINT ( 'NONE',  ( 42.88107685774368605, 18.83855087449469679, -13.00000000000000000 ) ) ;
#4686=DIRECTION ( 'NONE',  ( 1.000000000000000000, -6.124317834331790129E-17, 0.000000000000000000 ) ) ;
#4689=DIRECTION ( 'NONE',  ( -0.2306359803922080343, -0.9730401042858022320, -5.907067092757291018E-15 ) ) ;
#4691=VECTOR ( 'NONE', #19817, 1000.000000000000227 ) ;
#4694=AXIS2_PLACEMENT_3D ( 'NONE', #8883, #19320, #4718 ) ;
#4696=CARTESIAN_POINT ( 'NONE',  ( 117.0319250210129951, -13.02226701625849969, -18.89999999999999858 ) ) ;
#4697=DIRECTION ( 'NONE',  ( 6.124378941434239724E-17, -2.274246353359159970E-33, 1.000000000000000000 ) ) ;
#4698=ORIENTED_EDGE ( 'NONE', *, *, #2727, .T. ) ;
#4699=CARTESIAN_POINT ( 'NONE',  ( 113.4570673249340018, -28.10438863268850085, -2.700000000000000178 ) ) ;
#4708=CARTESIAN_POINT ( 'NONE',  ( 102.8131131701580046, 7.202356331284519797, 13.00000000000000000 ) ) ;
#4712=DESIGN_CONTEXT ( 'detailed design', #9897, 'design' ) ;
#4718=DIRECTION ( 'NONE',  ( 0.000000000000000000, -4.336808689942006376E-14, -1.000000000000000000 ) ) ;
#4724=DIRECTION ( 'NONE',  ( -0.2306359803922077290, -0.9730401042858024541, 0.000000000000000000 ) ) ;
#4735=EDGE_CURVE ( 'NONE', #2908, #1005, #1990, .T. ) ;
#4739=ORIENTED_EDGE ( 'NONE', *, *, #17674, .F. ) ;
#4754=EDGE_LOOP ( 'NONE', ( #13863, #18869, #4617, #2449 ) ) ;
#4757=DIRECTION ( 'NONE',  ( 0.9730401042858024541, -0.2306359803922080898, -5.959266323858942451E-17 ) ) ;
#4759=CYLINDRICAL_SURFACE ( 'NONE', #20988, 2.066999999999999726 ) ;
#4762=EDGE_CURVE ( 'NONE', #10345, #21559, #2030, .T. ) ;
#4766=CARTESIAN_POINT ( 'NONE',  ( 55.46237324781409939, -8.294657213477510282, -13.00000000000000000 ) ) ;
#4783=DIRECTION ( 'NONE',  ( 0.2306359803922080620, 0.9730401042858023430, 2.088419338574010618E-14 ) ) ;
#4784=DIRECTION ( 'NONE',  ( -0.9730401042858022320, 0.2306359803922080343, -2.823631968772345358E-31 ) ) ;
#4792=CARTESIAN_POINT ( 'NONE',  ( 51.98156320189720958, 17.12649442102254937, 13.00000000000000000 ) ) ;
#4794=DIRECTION ( 'NONE',  ( -0.9730401042858022320, 0.2306359803922080343, 5.959266323858941219E-17 ) ) ;
#4797=AXIS2_PLACEMENT_3D ( 'NONE', #2953, #16635, #6285 ) ;
#4806=FACE_OUTER_BOUND ( 'NONE', #7628, .T. ) ;
#4810=CARTESIAN_POINT ( 'NONE',  ( 96.33985310849000427, -20.10796027570521716, -13.00000000000000000 ) ) ;
#4812=AXIS2_PLACEMENT_3D ( 'NONE', #4594, #2819, #7810 ) ;
#4818=DIRECTION ( 'NONE',  ( -0.9730401042858022320, 0.2306359803922080343, 5.959266323858941219E-17 ) ) ;
#4820=EDGE_LOOP ( 'NONE', ( #18920, #9762 ) ) ;
#4830=DIRECTION ( 'NONE',  ( -0.9730401042858024541, 0.2306359803922080898, 5.959266323858222616E-17 ) ) ;
#4844=CIRCLE ( 'NONE', #4083, 2.066999999999999726 ) ;
#4847=ORIENTED_EDGE ( 'NONE', *, *, #5199, .T. ) ;
#4850=VERTEX_POINT ( 'NONE', #3790 ) ;
#4851=VECTOR ( 'NONE', #10327, 1000.000000000000227 ) ;
#4861=ORIENTED_EDGE ( 'NONE', *, *, #9372, .T. ) ;
#4863=ORIENTED_EDGE ( 'NONE', *, *, #12261, .F. ) ;
#4865=ORIENTED_EDGE ( 'NONE', *, *, #13206, .T. ) ;
#4868=VECTOR ( 'NONE', #3701, 1000.000000000000000 ) ;
#4871=DIRECTION ( 'NONE',  ( -0.9730401042858022320, 0.2306359803922080343, 5.959266323858941219E-17 ) ) ;
#4877=FACE_BOUND ( 'NONE', #12406, .T. ) ;
#4878=ADVANCED_FACE ( 'NONE', ( #19726 ), #10726, .F. ) ;
#4879=EDGE_CURVE ( 'NONE', #12948, #11681, #18597, .T. ) ;
#4890=DIRECTION ( 'NONE',  ( 0.2306359803922094498, 0.9730401042858018990, 0.000000000000000000 ) ) ;
#4901=EDGE_CURVE ( 'NONE', #2029, #12414, #10959, .T. ) ;
#4903=DIRECTION ( 'NONE',  ( -3.469446951953605354E-14, -1.084202172485501657E-13, 1.000000000000000000 ) ) ;
#4910=DIRECTION ( 'NONE',  ( 0.2306359803922085339, 0.9730401042858022320, 0.000000000000000000 ) ) ;
#4912=DIRECTION ( 'NONE',  ( 0.2306359803922085339, 0.9730401042858022320, 0.000000000000000000 ) ) ;
#4915=ORIENTED_EDGE ( 'NONE', *, *, #11446, .F. ) ;
#4920=ORIENTED_EDGE ( 'NONE', *, *, #13173, .T. ) ;
#4924=ORIENTED_EDGE ( 'NONE', *, *, #2972, .T. ) ;
#4925=VECTOR ( 'NONE', #18180, 1000.000000000000227 ) ;
#4926=DIRECTION ( 'NONE',  ( -0.9730401042858024541, 0.2306359803922080898, 5.959266323858711956E-17 ) ) ;
#4927=ORIENTED_EDGE ( 'NONE', *, *, #9729, .T. ) ;
#4929=AXIS2_PLACEMENT_3D ( 'NONE', #23216, #4943, #17883 ) ;
#4943=DIRECTION ( 'NONE',  ( -0.9730401042858024541, 0.2306359803922080898, 5.959266323858952312E-17 ) ) ;
#4975=CARTESIAN_POINT ( 'NONE',  ( 45.07211867146960316, 28.08243186520980217, -10.02499999999999858 ) ) ;
#4980=CARTESIAN_POINT ( 'NONE',  ( 39.83668191656649782, 5.994421497922090225, -18.89999999999999858 ) ) ;
#4981=EDGE_LOOP ( 'NONE', ( #12812, #13566, #4487, #11197 ) ) ;
#4985=ORIENTED_EDGE ( 'NONE', *, *, #23434, .T. ) ;
#4992=CIRCLE ( 'NONE', #20917, 2.066999999999999726 ) ;
#4997=CARTESIAN_POINT ( 'NONE',  ( 103.2898377416287303, 9.213630226843287474, -13.00000000000000000 ) ) ;
#5003=DIRECTION ( 'NONE',  ( 0.2306359803922080898, 0.9730401042858024541, -2.572202231434325988E-16 ) ) ;
#5023=CARTESIAN_POINT ( 'NONE',  ( 117.1241794131700118, -12.63305097454430026, 15.90000000000000036 ) ) ;
#5034=APPLICATION_CONTEXT ( 'configuration controlled 3d designs of mechanical parts and assemblies' ) ;
#5036=FACE_OUTER_BOUND ( 'NONE', #10525, .T. ) ;
#5056=LINE ( 'NONE', #12415, #9108 ) ;
#5060=CARTESIAN_POINT ( 'NONE',  ( 118.5079952955230027, -6.794810348829399160, 15.50000000000000000 ) ) ;
#5065=VECTOR ( 'NONE', #19782, 999.9999999999998863 ) ;
#5072=ORIENTED_EDGE ( 'NONE', *, *, #13795, .T. ) ;
#5076=EDGE_CURVE ( 'NONE', #503, #8379, #18659, .T. ) ;
#5078=CARTESIAN_POINT ( 'NONE',  ( 113.2956221386590130, -28.78551670568859677, -3.100000000000000089 ) ) ;
#5079=VERTEX_POINT ( 'NONE', #18544 ) ;
#5090=CIRCLE ( 'NONE', #18360, 2.999999999999999556 ) ;
#5093=LINE ( 'NONE', #13764, #21361 ) ;
#5097=AXIS2_PLACEMENT_3D ( 'NONE', #10693, #7013, #5318 ) ;
#5104=ORIENTED_EDGE ( 'NONE', *, *, #752, .T. ) ;
#5106=VERTEX_POINT ( 'NONE', #19004 ) ;
#5109=VERTEX_POINT ( 'NONE', #8088 ) ;
#5119=CARTESIAN_POINT ( 'NONE',  ( 105.8171986446039909, -20.23006919877430221, 13.00000000000000000 ) ) ;
#5121=EDGE_LOOP ( 'NONE', ( #17058, #23390, #16381, #7156 ) ) ;
#5123=PLANE ( 'NONE',  #7490 ) ;
#5124=AXIS2_PLACEMENT_3D ( 'NONE', #18642, #2356, #6278 ) ;
#5141=DIRECTION ( 'NONE',  ( 0.2306359803922080898, 0.9730401042858024541, -2.572202231434325988E-16 ) ) ;
#5153=ORIENTED_EDGE ( 'NONE', *, *, #16481, .T. ) ;
#5154=CARTESIAN_POINT ( 'NONE',  ( 117.1011158151309957, -12.73035498497280038, 20.00000000000000000 ) ) ;
#5159=CARTESIAN_POINT ( 'NONE',  ( 39.76749112244880280, 5.702509466636288771, 15.90000000000000036 ) ) ;
#5166=VECTOR ( 'NONE', #21691, 1000.000000000000000 ) ;
#5169=ORIENTED_EDGE ( 'NONE', *, *, #17945, .F. ) ;
#5171=EDGE_CURVE ( 'NONE', #21047, #300, #23015, .T. ) ;
#5172=EDGE_CURVE ( 'NONE', #19198, #12333, #6067, .T. ) ;
#5183=ORIENTED_EDGE ( 'NONE', *, *, #96, .F. ) ;
#5186=ORIENTED_EDGE ( 'NONE', *, *, #20712, .F. ) ;
#5187=CIRCLE ( 'NONE', #4812, 0.4000000000000010214 ) ;
#5189=DIRECTION ( 'NONE',  ( 0.2306359803922083396, 0.9730401042858023430, 8.673617379884037996E-14 ) ) ;
#5198=VERTEX_POINT ( 'NONE', #21125 ) ;
#5199=EDGE_CURVE ( 'NONE', #9773, #6033, #13779, .T. ) ;
#5221=VECTOR ( 'NONE', #2066, 1000.000000000000227 ) ;
#5222=EDGE_CURVE ( 'NONE', #10345, #21109, #18214, .T. ) ;
#5224=FACE_BOUND ( 'NONE', #10101, .T. ) ;
#5230=CARTESIAN_POINT ( 'NONE',  ( 45.07211867146970263, 28.08243186520990164, 13.00000000000000000 ) ) ;
#5231=ORIENTED_EDGE ( 'NONE', *, *, #17043, .F. ) ;
#5236=ORIENTED_EDGE ( 'NONE', *, *, #5711, .T. ) ;
#5256=CARTESIAN_POINT ( 'NONE',  ( 40.45939906362549721, 8.621629779493760637, 3.888892445930440142E-14 ) ) ;
#5272=CARTESIAN_POINT ( 'NONE',  ( 113.2956221386590130, -28.78551670568849730, 3.100000000000000089 ) ) ;
#5288=EDGE_CURVE ( 'NONE', #6720, #13613, #20818, .T. ) ;
#5294=CARTESIAN_POINT ( 'NONE',  ( 52.05497947389309843, 22.85602965967900246, 3.416161896595049310E-14 ) ) ;
#5297=DIRECTION ( 'NONE',  ( -0.2306359803922080343, -0.9730401042858022320, 2.974717104243940401E-15 ) ) ;
#5305=ADVANCED_FACE ( 'NONE', ( #13135 ), #5530, .F. ) ;
#5308=ORIENTED_EDGE ( 'NONE', *, *, #11292, .F. ) ;
#5314=DIRECTION ( 'NONE',  ( -0.9730401042858024541, 0.2306359803922080898, 5.959266323858942451E-17 ) ) ;
#5318=DIRECTION ( 'NONE',  ( -0.2306359803922085339, -0.9730401042858022320, 0.000000000000000000 ) ) ;
#5319=CARTESIAN_POINT ( 'NONE',  ( 122.7747609327790030, 11.20643158045800014, -9.133960000000000079 ) ) ;
#5320=ORIENTED_EDGE ( 'NONE', *, *, #22912, .F. ) ;
#5324=ORIENTED_EDGE ( 'NONE', *, *, #498, .T. ) ;
#5336=CARTESIAN_POINT ( 'NONE',  ( 51.09971998237313784, 11.23812949209873935, 3.823728413317720161E-14 ) ) ;
#5342=DIRECTION ( 'NONE',  ( 2.471194949999149731E-15, 1.016744709403700171E-14, 1.000000000000000000 ) ) ;
#5350=ORIENTED_EDGE ( 'NONE', *, *, #1526, .F. ) ;
#5351=EDGE_LOOP ( 'NONE', ( #3583, #17772, #16976, #13733 ) ) ;
#5359=DIRECTION ( 'NONE',  ( 0.2306359803922076457, 0.9730401042858023430, 0.000000000000000000 ) ) ;
#5369=DIRECTION ( 'NONE',  ( 0.000000000000000000, -2.098117411679737831E-16, -1.000000000000000000 ) ) ;
#5391=AXIS2_PLACEMENT_3D ( 'NONE', #16415, #10872, #16187 ) ;
#5396=AXIS2_PLACEMENT_3D ( 'NONE', #13362, #22366, #22598 ) ;
#5413=ORIENTED_EDGE ( 'NONE', *, *, #4879, .T. ) ;
#5422=ORIENTED_EDGE ( 'NONE', *, *, #17971, .T. ) ;
#5423=LINE ( 'NONE', #61, #18141 ) ;
#5431=EDGE_CURVE ( 'NONE', #16449, #19011, #11014, .T. ) ;
#5440=DIRECTION ( 'NONE',  ( 0.2306359803922085339, 0.9730401042858022320, 0.000000000000000000 ) ) ;
#5467=LINE ( 'NONE', #18056, #12422 ) ;
#5479=EDGE_LOOP ( 'NONE', ( #16754, #20151, #11497, #19701 ) ) ;
#5490=DIRECTION ( 'NONE',  ( -0.9730401042858022320, 0.2306359803922080343, 5.959266323858941219E-17 ) ) ;
#5494=LINE ( 'NONE', #8840, #14416 ) ;
#5515=DIRECTION ( 'NONE',  ( 0.2306359803922080343, 0.9730401042858022320, 7.611545645953073104E-14 ) ) ;
#5519=LINE ( 'NONE', #7194, #9656 ) ;
#5522=LINE ( 'NONE', #11130, #21826 ) ;
#5530=CYLINDRICAL_SURFACE ( 'NONE', #11791, 2.066999999999997950 ) ;
#5531=ORIENTED_EDGE ( 'NONE', *, *, #4901, .T. ) ;
#5539=DIRECTION ( 'NONE',  ( -0.9730401042858024541, 0.2306359803922080898, 5.959266323858942451E-17 ) ) ;
#5540=CIRCLE ( 'NONE', #16917, 4.999999999999998224 ) ;
#5542=ORIENTED_EDGE ( 'NONE', *, *, #1906, .F. ) ;
#5546=DIRECTION ( 'NONE',  ( 0.9730401042858024541, -0.2306359803922080898, -5.959266323858942451E-17 ) ) ;
#5552=FACE_OUTER_BOUND ( 'NONE', #22301, .T. ) ;
#5565=ADVANCED_FACE ( 'NONE', ( #15492 ), #22722, .T. ) ;
#5568=AXIS2_PLACEMENT_3D ( 'NONE', #20940, #6818, #3129 ) ;
#5576=CARTESIAN_POINT ( 'NONE',  ( 122.4288069621910040, 9.746871424029221131, -10.02499999999999858 ) ) ;
#5584=EDGE_CURVE ( 'NONE', #18769, #2719, #9502, .T. ) ;
#5585=AXIS2_PLACEMENT_3D ( 'NONE', #5159, #12418, #19652 ) ;
#5587=ORIENTED_EDGE ( 'NONE', *, *, #21082, .F. ) ;
#5588=FACE_OUTER_BOUND ( 'NONE', #11782, .T. ) ;
#5590=CARTESIAN_POINT ( 'NONE',  ( 41.08211621068439712, 11.24883806106539907, 19.59999999999999787 ) ) ;
#5597=EDGE_CURVE ( 'NONE', #22958, #13304, #20952, .T. ) ;
#5599=VECTOR ( 'NONE', #18173, 1000.000000000000000 ) ;
#5614=ORIENTED_EDGE ( 'NONE', *, *, #10780, .F. ) ;
#5628=CARTESIAN_POINT ( 'NONE',  ( 117.1933702072879981, -12.34113894325840022, 18.89999999999999858 ) ) ;
#5633=DIRECTION ( 'NONE',  ( 0.000000000000000000, 0.000000000000000000, 1.000000000000000000 ) ) ;
#5641=LINE ( 'NONE', #12890, #2379 ) ;
#5674=DIRECTION ( 'NONE',  ( 0.000000000000000000, 0.000000000000000000, 1.000000000000000000 ) ) ;
#5685=ORIENTED_EDGE ( 'NONE', *, *, #12479, .T. ) ;
#5689=ORIENTED_EDGE ( 'NONE', *, *, #11292, .T. ) ;
#5690=ORIENTED_EDGE ( 'NONE', *, *, #1280, .F. ) ;
#5705=PLANE ( 'NONE',  #17078 ) ;
#5711=EDGE_CURVE ( 'NONE', #9929, #18262, #20447, .T. ) ;
#5744=CARTESIAN_POINT ( 'NONE',  ( 113.4570673249340018, -28.10438863268850085, -3.399999999999949729 ) ) ;
#5746=CARTESIAN_POINT ( 'NONE',  ( 113.2033677465029911, -29.17473274740279976, 13.00000000000000000 ) ) ;
#5760=ORIENTED_EDGE ( 'NONE', *, *, #20798, .T. ) ;
#5768=VECTOR ( 'NONE', #312, 1000.000000000000000 ) ;
#5770=DIRECTION ( 'NONE',  ( 0.2306359803922078122, 0.9730401042858023430, 2.478176394252582127E-15 ) ) ;
#5772=LINE ( 'NONE', #10603, #14129 ) ;
#5775=AXIS2_PLACEMENT_3D ( 'NONE', #7755, #16639, #20453 ) ;
#5781=EDGE_CURVE ( 'NONE', #1005, #2908, #12143, .T. ) ;
#5786=CARTESIAN_POINT ( 'NONE',  ( 118.6002496876800052, -6.405594307115080710, -18.89999999999999858 ) ) ;
#5789=CARTESIAN_POINT ( 'NONE',  ( 39.67523673029199927, 5.313293424922060026, -18.89999999999999858 ) ) ;
#5792=DIRECTION ( 'NONE',  ( 0.1630842657209385649, 0.6880432561069587116, 0.7071067811865449082 ) ) ;
#5794=ORIENTED_EDGE ( 'NONE', *, *, #21285, .F. ) ;
#5796=ADVANCED_FACE ( 'NONE', ( #7072 ), #12187, .F. ) ;
#5813=AXIS2_PLACEMENT_3D ( 'NONE', #22476, #6224, #19047 ) ;
#5817=LINE ( 'NONE', #11055, #10760 ) ;
#5838=CARTESIAN_POINT ( 'NONE',  ( 118.5079952955235996, -6.794810348829486202, 3.447633465585020886E-14 ) ) ;
#5855=VECTOR ( 'NONE', #14118, 1000.000000000000000 ) ;
#5856=FACE_OUTER_BOUND ( 'NONE', #5121, .T. ) ;
#5864=CARTESIAN_POINT ( 'NONE',  ( 118.6002496876800052, -6.405594307115070052, -15.90000000000000036 ) ) ;
#5887=FACE_OUTER_BOUND ( 'NONE', #21368, .T. ) ;
#5888=EDGE_CURVE ( 'NONE', #4401, #14881, #12526, .T. ) ;
#5897=DIRECTION ( 'NONE',  ( -0.2306359803922085339, -0.9730401042858022320, 0.000000000000000000 ) ) ;
#5900=EDGE_LOOP ( 'NONE', ( #13710, #1197, #20809, #10641 ) ) ;
#5903=ORIENTED_EDGE ( 'NONE', *, *, #15808, .T. ) ;
#5911=CARTESIAN_POINT ( 'NONE',  ( 105.8171986446039909, -20.23006919877430221, -13.00000000000000000 ) ) ;
#5912=ORIENTED_EDGE ( 'NONE', *, *, #14280, .T. ) ;
#5925=CARTESIAN_POINT ( 'NONE',  ( 111.8137341348020044, 5.068973512656540059, -13.00000000000000000 ) ) ;
#5927=VECTOR ( 'NONE', #16281, 1000.000000000000000 ) ;
#5929=ORIENTED_EDGE ( 'NONE', *, *, #1133, .F. ) ;
#5933=PLANE ( 'NONE',  #17222 ) ;
#5940=EDGE_LOOP ( 'NONE', ( #10717, #20748, #12358, #11533 ) ) ;
#5953=CARTESIAN_POINT ( 'NONE',  ( 122.4288069621910040, 9.746871424029221131, -10.02499999999999858 ) ) ;
#5959=VERTEX_POINT ( 'NONE', #18342 ) ;
#5960=AXIS2_PLACEMENT_3D ( 'NONE', #5272, #12534, #9314 ) ;
#5971=CIRCLE ( 'NONE', #9015, 2.066999999999999726 ) ;
#5981=AXIS2_PLACEMENT_3D ( 'NONE', #13693, #6095, #8006 ) ;
#5982=VECTOR ( 'NONE', #11356, 1000.000000000000227 ) ;
#5991=LINE ( 'NONE', #9696, #1380 ) ;
#6001=CARTESIAN_POINT ( 'NONE',  ( 113.4570673249340018, -28.10438863268850085, -2.700000000000000178 ) ) ;
#6007=DIRECTION ( 'NONE',  ( 0.9730401042858023430, -0.2306359803922080620, -5.959266323858946149E-17 ) ) ;
#6020=LINE ( 'NONE', #13619, #3300 ) ;
#6029=EDGE_CURVE ( 'NONE', #6605, #19111, #9852, .T. ) ;
#6033=VERTEX_POINT ( 'NONE', #7875 ) ;
#6040=CARTESIAN_POINT ( 'NONE',  ( 113.2033677465029911, -29.17473274740279976, 3.100000000000039613 ) ) ;
#6046=ORIENTED_EDGE ( 'NONE', *, *, #8571, .T. ) ;
#6048=CARTESIAN_POINT ( 'NONE',  ( 55.46237324781409939, -8.294657213477510282, 13.00000000000000000 ) ) ;
#6063=CARTESIAN_POINT ( 'NONE',  ( 102.3363885986873356, 5.191082435725784983, -13.00000000000000000 ) ) ;
#6064=DIRECTION ( 'NONE',  ( 0.2306359803922076457, 0.9730401042858025651, -1.412237191019970710E-17 ) ) ;
#6066=AXIS2_PLACEMENT_3D ( 'NONE', #12081, #17039, #8265 ) ;
#6067=CIRCLE ( 'NONE', #3406, 2.066999999999999726 ) ;
#6075=ORIENTED_EDGE ( 'NONE', *, *, #22865, .T. ) ;
#6085=ORIENTED_EDGE ( 'NONE', *, *, #20028, .T. ) ;
#6092=CARTESIAN_POINT ( 'NONE',  ( 118.5079952955230027, -6.794810348829379620, -15.90000000000000036 ) ) ;
#6095=DIRECTION ( 'NONE',  ( -0.9730401042858024541, 0.2306359803922080898, 5.959266323858942451E-17 ) ) ;
#6103=CARTESIAN_POINT ( 'NONE',  ( 114.1489752661110089, -25.18526831983109915, 3.000000000000000000 ) ) ;
#6131=ORIENTED_EDGE ( 'NONE', *, *, #18854, .T. ) ;
#6133=ORIENTED_EDGE ( 'NONE', *, *, #14312, .F. ) ;
#6145=ORIENTED_EDGE ( 'NONE', *, *, #19519, .F. ) ;
#6155=CARTESIAN_POINT ( 'NONE',  ( 118.6002496876800052, -6.405594307115060282, 15.90000000000000036 ) ) ;
#6167=EDGE_LOOP ( 'NONE', ( #5690, #1658, #6527, #14488 ) ) ;
#6193=AXIS2_PLACEMENT_3D ( 'NONE', #5925, #10829, #7251 ) ;
#6200=CIRCLE ( 'NONE', #21369, 2.066999999999998394 ) ;
#6204=CONICAL_SURFACE ( 'NONE', #5813, 2.283500000000000529, 0.7853981633974469467 ) ;
#6212=ORIENTED_EDGE ( 'NONE', *, *, #13624, .T. ) ;
#6214=FACE_BOUND ( 'NONE', #3987, .T. ) ;
#6224=DIRECTION ( 'NONE',  ( 0.9730401042858024541, -0.2306359803922080898, -5.959266323858942451E-17 ) ) ;
#6270=ORIENTED_EDGE ( 'NONE', *, *, #10718, .T. ) ;
#6278=DIRECTION ( 'NONE',  ( -0.2306359803922076457, -0.9730401042858025651, 0.000000000000000000 ) ) ;
#6283=ORIENTED_EDGE ( 'NONE', *, *, #5171, .T. ) ;
#6285=DIRECTION ( 'NONE',  ( 0.000000000000000000, 4.336808689942006376E-14, 1.000000000000000000 ) ) ;
#6289=DIRECTION ( 'NONE',  ( -0.9730401042858023430, 0.2306359803922080620, 5.959266323858944916E-17 ) ) ;
#6290=DIRECTION ( 'NONE',  ( -0.2306359803922053142, -0.9730401042858028982, 0.000000000000000000 ) ) ;
#6297=AXIS2_PLACEMENT_3D ( 'NONE', #3382, #12669, #16549 ) ;
#6305=EDGE_CURVE ( 'NONE', #3952, #7758, #6934, .T. ) ;
#6308=DIRECTION ( 'NONE',  ( 0.2306359803922076457, 0.9730401042858023430, -1.412237191019970710E-17 ) ) ;
#6313=EDGE_LOOP ( 'NONE', ( #15568, #19995, #22501, #2766 ) ) ;
#6323=ORIENTED_EDGE ( 'NONE', *, *, #22689, .F. ) ;
#6328=EDGE_CURVE ( 'NONE', #9834, #6033, #2991, .T. ) ;
#6331=EDGE_CURVE ( 'NONE', #5079, #3196, #15252, .T. ) ;
#6334=EDGE_CURVE ( 'NONE', #8816, #3586, #8058, .T. ) ;
#6345=CARTESIAN_POINT ( 'NONE',  ( 41.15130700480209924, 11.54075009235119964, -15.50000000000000000 ) ) ;
#6348=CYLINDRICAL_SURFACE ( 'NONE', #5396, 0.3999999999999982458 ) ;
#6354=ORIENTED_EDGE ( 'NONE', *, *, #15483, .T. ) ;
#6358=AXIS2_PLACEMENT_3D ( 'NONE', #20977, #22975, #17661 ) ;
#6364=CARTESIAN_POINT ( 'NONE',  ( 43.66832999130209458, 21.22121844545429781, 13.00000000000000000 ) ) ;
#6383=ORIENTED_EDGE ( 'NONE', *, *, #12770, .F. ) ;
#6397=ORIENTED_EDGE ( 'NONE', *, *, #22919, .T. ) ;
#6410=VERTEX_POINT ( 'NONE', #7394 ) ;
#6419=CARTESIAN_POINT ( 'NONE',  ( 118.5079952955230027, -6.794810348829359192, -15.50000000000000000 ) ) ;
#6437=FACE_OUTER_BOUND ( 'NONE', #4981, .T. ) ;
#6439=ORIENTED_EDGE ( 'NONE', *, *, #7656, .F. ) ;
#6441=LINE ( 'NONE', #12051, #9237 ) ;
#6446=AXIS2_PLACEMENT_3D ( 'NONE', #17629, #6704, #4910 ) ;
#6448=DIRECTION ( 'NONE',  ( -0.9730401042858024541, 0.2306359803922080898, 5.959266323858942451E-17 ) ) ;
#6454=ADVANCED_FACE ( 'NONE', ( #5588 ), #8885, .F. ) ;
#6464=CARTESIAN_POINT ( 'NONE',  ( 121.3909450504253584, 5.368190954742481757, -13.00000000000000000 ) ) ;
#6470=CARTESIAN_POINT ( 'NONE',  ( 117.1011158151309957, -12.73035498497280038, -19.59999999999999787 ) ) ;
#6480=CYLINDRICAL_SURFACE ( 'NONE', #3526, 0.3999999999999982458 ) ;
#6486=FACE_OUTER_BOUND ( 'NONE', #4311, .T. ) ;
#6487=AXIS2_PLACEMENT_3D ( 'NONE', #17663, #3275, #1364 ) ;
#6501=CARTESIAN_POINT ( 'NONE',  ( 45.41807264205800010, 29.54199202163849947, 9.133960000000000079 ) ) ;
#6524=DIRECTION ( 'NONE',  ( -0.2306359803922094498, -0.9730401042858020100, 1.412237191019847142E-17 ) ) ;
#6527=ORIENTED_EDGE ( 'NONE', *, *, #4762, .T. ) ;
#6538=VECTOR ( 'NONE', #2586, 1000.000000000000000 ) ;
#6539=AXIS2_PLACEMENT_3D ( 'NONE', #16164, #562, #18400 ) ;
#6564=DIRECTION ( 'NONE',  ( -0.9730401042858022320, 0.2306359803922080343, 5.959266323858941219E-17 ) ) ;
#6574=VERTEX_POINT ( 'NONE', #18434 ) ;
#6605=VERTEX_POINT ( 'NONE', #11563 ) ;
#6611=CARTESIAN_POINT ( 'NONE',  ( 35.84667945578129888, -10.83917230622230043, 3.100000000000039613 ) ) ;
#6613=EDGE_CURVE ( 'NONE', #14262, #23458, #2621, .T. ) ;
#6616=CIRCLE ( 'NONE', #19883, 2.066999999999999726 ) ;
#6627=LINE ( 'NONE', #19318, #12976 ) ;
#6630=FACE_OUTER_BOUND ( 'NONE', #14986, .T. ) ;
#6635=DIRECTION ( 'NONE',  ( 0.2306359803922080343, 0.9730401042858022320, -1.412237191019910313E-17 ) ) ;
#6638=CARTESIAN_POINT ( 'NONE',  ( 52.93501234483849771, 21.14904221214005631, -13.00000000000000000 ) ) ;
#6641=EDGE_CURVE ( 'NONE', #14346, #300, #17103, .T. ) ;
#6647=DIRECTION ( 'NONE',  ( -0.9730401042858022320, 0.2306359803922080343, 5.959266323858941219E-17 ) ) ;
#6649=AXIS2_PLACEMENT_3D ( 'NONE', #8410, #17207, #2706 ) ;
#6658=ORIENTED_EDGE ( 'NONE', *, *, #18798, .F. ) ;
#6664=CIRCLE ( 'NONE', #5124, 2.499999999999999112 ) ;
#6672=DIRECTION ( 'NONE',  ( -0.9730401042858022320, 0.2306359803922080343, 5.959266323858941219E-17 ) ) ;
#6685=CARTESIAN_POINT ( 'NONE',  ( 113.2033677465029911, -29.17473274740279976, 3.100000000000039613 ) ) ;
#6690=DIRECTION ( 'NONE',  ( 0.2306359803922080620, 0.9730401042858023430, -5.935311836577789915E-15 ) ) ;
#6692=EDGE_CURVE ( 'NONE', #8196, #19011, #15202, .T. ) ;
#6704=DIRECTION ( 'NONE',  ( -0.9730401042858024541, 0.2306359803922080898, 5.959266323858942451E-17 ) ) ;
#6718=ORIENTED_EDGE ( 'NONE', *, *, #684, .F. ) ;
#6720=VERTEX_POINT ( 'NONE', #3084 ) ;
#6721=DIRECTION ( 'NONE',  ( 0.2306359803921919083, 0.9730401042858062288, 8.673617379884073337E-14 ) ) ;
#6729=DIRECTION ( 'NONE',  ( -0.2306359803921919083, -0.9730401042858062288, 0.000000000000000000 ) ) ;
#6738=AXIS2_PLACEMENT_3D ( 'NONE', #18202, #12518, #12855 ) ;
#6740=DIRECTION ( 'NONE',  ( 0.2306359803922076457, 0.9730401042858025651, 0.000000000000000000 ) ) ;
#6744=VECTOR ( 'NONE', #1353, 1000.000000000000114 ) ;
#6745=FACE_OUTER_BOUND ( 'NONE', #7904, .T. ) ;
#6755=CIRCLE ( 'NONE', #12814, 2.066999999999999726 ) ;
#6760=LINE ( 'NONE', #21108, #18336 ) ;
#6765=CIRCLE ( 'NONE', #22654, 2.066999999999999726 ) ;
#6768=ORIENTED_EDGE ( 'NONE', *, *, #10780, .T. ) ;
#6773=CIRCLE ( 'NONE', #14335, 2.066999999999999726 ) ;
#6782=CIRCLE ( 'NONE', #4492, 2.066999999999999726 ) ;
#6788=VECTOR ( 'NONE', #15562, 1000.000000000000227 ) ;
#6791=DIRECTION ( 'NONE',  ( 6.124378941434239724E-17, -2.274246353359159970E-33, 1.000000000000000000 ) ) ;
#6809=CARTESIAN_POINT ( 'NONE',  ( 114.8178196092480050, -22.36345201740219935, -20.00000000000000000 ) ) ;
#6818=DIRECTION ( 'NONE',  ( -0.2306359803922080620, -0.9730401042858023430, -3.574477303645826527E-15 ) ) ;
#6819=EDGE_CURVE ( 'NONE', #16084, #11146, #1300, .T. ) ;
#6845=DIRECTION ( 'NONE',  ( -0.9730401042858024541, 0.2306359803922080898, 5.959266323858942451E-17 ) ) ;
#6846=VECTOR ( 'NONE', #22909, 1000.000000000000227 ) ;
#6847=ORIENTED_EDGE ( 'NONE', *, *, #8696, .T. ) ;
#6876=ORIENTED_EDGE ( 'NONE', *, *, #14220, .T. ) ;
#6883=CARTESIAN_POINT ( 'NONE',  ( 122.7747609327790030, 11.20643158045800014, 9.133960000000000079 ) ) ;
#6892=ORIENTED_EDGE ( 'NONE', *, *, #626, .T. ) ;
#6912=DIRECTION ( 'NONE',  ( 1.164423685541379998E-14, 4.938475812832819565E-14, -1.000000000000000000 ) ) ;
#6913=DIRECTION ( 'NONE',  ( 0.000000000000000000, -4.196234823359475661E-16, -1.000000000000000000 ) ) ;
#6926=CARTESIAN_POINT ( 'NONE',  ( 112.5523895830310011, 2.765522746992189695, 3.181688650527689809E-14 ) ) ;
#6931=AXIS2_PLACEMENT_3D ( 'NONE', #8464, #22932, #17610 ) ;
#6933=CARTESIAN_POINT ( 'NONE',  ( 41.08211621068439712, 11.24883806106539907, -18.89999999999999858 ) ) ;
#6934=CIRCLE ( 'NONE', #8829, 0.4000000000000010214 ) ;
#6942=CARTESIAN_POINT ( 'NONE',  ( 112.6956120935900003, 3.369770385951889935, 3.165715546043859906E-14 ) ) ;
#6949=CARTESIAN_POINT ( 'NONE',  ( 43.45766680872420551, 21.27115113520929768, 13.00000000000000000 ) ) ;
#6963=FACE_OUTER_BOUND ( 'NONE', #21644, .T. ) ;
#6966=AXIS2_PLACEMENT_3D ( 'NONE', #858, #20811, #11815 ) ;
#6974=AXIS2_PLACEMENT_3D ( 'NONE', #22999, #8896, #1500 ) ;
#6982=DIRECTION ( 'NONE',  ( 0.2306359803922080620, 0.9730401042858023430, -1.046328025073550694E-14 ) ) ;
#6985=CARTESIAN_POINT ( 'NONE',  ( 118.6002496876800052, -6.405594307115129560, 18.89999999999999858 ) ) ;
#6991=ORIENTED_EDGE ( 'NONE', *, *, #10006, .F. ) ;
#6995=DIRECTION ( 'NONE',  ( 4.328311834315510110E-15, 1.851928590941880236E-14, -1.000000000000000000 ) ) ;
#6998=CARTESIAN_POINT ( 'NONE',  ( 50.90756547144185618, 18.01515514085710734, 2.067000000000035254 ) ) ;
#7010=DIRECTION ( 'NONE',  ( -0.9730401042858024541, 0.2306359803922080898, 5.959266323858942451E-17 ) ) ;
#7011=DIRECTION ( 'NONE',  ( -0.2306359803922066187, -0.9730401042858026761, 0.000000000000000000 ) ) ;
#7013=DIRECTION ( 'NONE',  ( 0.9730401042858024541, -0.2306359803922080898, -5.959266323858942451E-17 ) ) ;
#7015=EDGE_LOOP ( 'NONE', ( #5169, #1925, #15429, #6718 ) ) ;
#7031=CARTESIAN_POINT ( 'NONE',  ( 96.81657767996070163, -18.09668638014640152, 13.00000000000000000 ) ) ;
#7051=CARTESIAN_POINT ( 'NONE',  ( 114.9405074087380001, 12.84085624101770051, 2.915350241847199977E-14 ) ) ;
#7054=DIRECTION ( 'NONE',  ( -0.2306359803922076734, -0.9730401042858024541, 1.412237191019896754E-17 ) ) ;
#7061=DIRECTION ( 'NONE',  ( 0.9730401042858024541, -0.2306359803922080898, -5.959266323858942451E-17 ) ) ;
#7072=FACE_OUTER_BOUND ( 'NONE', #1730, .T. ) ;
#7073=EDGE_CURVE ( 'NONE', #2422, #563, #1993, .T. ) ;
#7081=FACE_OUTER_BOUND ( 'NONE', #10173, .T. ) ;
#7100=CARTESIAN_POINT ( 'NONE',  ( 41.08211621068439712, 11.24883806106539907, -19.59999999999999787 ) ) ;
#7106=DIRECTION ( 'NONE',  ( 0.2306359803922085339, 0.9730401042858022320, 0.000000000000000000 ) ) ;
#7113=AXIS2_PLACEMENT_3D ( 'NONE', #7766, #10998, #11473 ) ;
#7119=VERTEX_POINT ( 'NONE', #7582 ) ;
#7156=ORIENTED_EDGE ( 'NONE', *, *, #6641, .T. ) ;
#7161=CARTESIAN_POINT ( 'NONE',  ( 113.2033677465029911, -29.17473274740279976, -13.00000000000000000 ) ) ;
#7162=ADVANCED_FACE ( 'NONE', ( #12088 ), #6480, .F. ) ;
#7164=CIRCLE ( 'NONE', #15880, 4.999999999999998224 ) ;
#7177=ORIENTED_EDGE ( 'NONE', *, *, #8477, .T. ) ;
#7183=VERTEX_POINT ( 'NONE', #11973 ) ;
#7192=CARTESIAN_POINT ( 'NONE',  ( 113.2956221386590130, -28.78551670568849730, 2.700000000000000178 ) ) ;
#7194=CARTESIAN_POINT ( 'NONE',  ( 120.8143550994449953, 2.935590694028619829, -20.00000000000000000 ) ) ;
#7196=FACE_OUTER_BOUND ( 'NONE', #4395, .T. ) ;
#7199=ORIENTED_EDGE ( 'NONE', *, *, #595, .T. ) ;
#7205=CARTESIAN_POINT ( 'NONE',  ( 114.9904400984929254, 13.05151942359561801, -2.500000000000011990 ) ) ;
#7228=CARTESIAN_POINT ( 'NONE',  ( 43.87899317387989839, 21.17128575569940097, -13.00000000000000000 ) ) ;
#7232=DIRECTION ( 'NONE',  ( -0.2306359803922053142, -0.9730401042858028982, 0.000000000000000000 ) ) ;
#7251=DIRECTION ( 'NONE',  ( -0.2306359803922053697, -0.9730401042858028982, 0.000000000000000000 ) ) ;
#7268=EDGE_LOOP ( 'NONE', ( #309, #3832, #5760, #23366 ) ) ;
#7269=EDGE_LOOP ( 'NONE', ( #19096, #3096, #22523, #12865 ) ) ;
#7277=DIRECTION ( 'NONE',  ( -0.9730401042858022320, 0.2306359803922080343, 5.959266323858951079E-17 ) ) ;
#7283=DIRECTION ( 'NONE',  ( 0.9730401042858024541, -0.2306359803922080898, -5.959266323858912869E-17 ) ) ;
#7287=ADVANCED_FACE ( 'NONE', ( #15503 ), #1356, .T. ) ;
#7288=CARTESIAN_POINT ( 'NONE',  ( 113.2956221386590130, -28.78551670568849730, 3.100000000000000089 ) ) ;
#7303=VECTOR ( 'NONE', #10027, 1000.000000000000000 ) ;
#7306=AXIS2_PLACEMENT_3D ( 'NONE', #9092, #16324, #16666 ) ;
#7309=FACE_OUTER_BOUND ( 'NONE', #7499, .T. ) ;
#7335=DIRECTION ( 'NONE',  ( 0.1187863113461967018, 0.5011527021216418687, 0.8571673007021100021 ) ) ;
#7342=AXIS2_PLACEMENT_3D ( 'NONE', #13303, #20425, #14962 ) ;
#7346=LINE ( 'NONE', #14579, #12111 ) ;
#7349=VECTOR ( 'NONE', #21400, 1000.000000000000227 ) ;
#7350=CARTESIAN_POINT ( 'NONE',  ( 117.1933702072879981, -12.34113894325849969, 19.59999999999999787 ) ) ;
#7353=ORIENTED_EDGE ( 'NONE', *, *, #16219, .T. ) ;
#7361=ADVANCED_FACE ( 'NONE', ( #7081 ), #157, .T. ) ;
#7378=EDGE_LOOP ( 'NONE', ( #8993, #6075, #3083, #2619 ) ) ;
#7381=DIRECTION ( 'NONE',  ( 6.124378941434239724E-17, -2.274246353359159970E-33, 1.000000000000000000 ) ) ;
#7393=EDGE_LOOP ( 'NONE', ( #10814, #20976, #17516, #13297 ) ) ;
#7394=CARTESIAN_POINT ( 'NONE',  ( 113.2033677465029911, -29.17473274740279976, 13.00000000000000000 ) ) ;
#7397=DIRECTION ( 'NONE',  ( 1.173102895937339952E-16, 2.365413804416879953E-16, 1.000000000000000000 ) ) ;
#7402=ADVANCED_FACE ( 'NONE', ( #7309 ), #18334, .F. ) ;
#7416=CARTESIAN_POINT ( 'NONE',  ( 113.4570673249340018, -28.10438863268850085, 3.399999999999999911 ) ) ;
#7421=CARTESIAN_POINT ( 'NONE',  ( 46.93847685464109531, -4.150000499290836586, -13.00000000000000000 ) ) ;
#7424=DIRECTION ( 'NONE',  ( -0.2306359803922066187, -0.9730401042858026761, 0.000000000000000000 ) ) ;
#7427=DIRECTION ( 'NONE',  ( -0.9730401042858022320, 0.2306359803922080343, 5.959266323858941219E-17 ) ) ;
#7435=CIRCLE ( 'NONE', #6297, 2.500000000000000000 ) ;
#7441=EDGE_LOOP ( 'NONE', ( #16614, #17580, #11613, #16671 ) ) ;
#7453=EDGE_CURVE ( 'NONE', #20142, #6574, #14548, .T. ) ;
#7458=CARTESIAN_POINT ( 'NONE',  ( 41.08211621068439712, 11.24883806106539907, -18.89999999999999858 ) ) ;
#7467=ORIENTED_EDGE ( 'NONE', *, *, #22139, .T. ) ;
#7487=DIRECTION ( 'NONE',  ( -0.9730401042858024541, 0.2306359803922080898, 5.959266323858942451E-17 ) ) ;
#7490=AXIS2_PLACEMENT_3D ( 'NONE', #3577, #20061, #7381 ) ;
#7492=EDGE_LOOP ( 'NONE', ( #13335, #5231, #7177, #1360 ) ) ;
#7494=ORIENTED_EDGE ( 'NONE', *, *, #4762, .F. ) ;
#7499=EDGE_LOOP ( 'NONE', ( #22034, #2149, #8225, #9831 ) ) ;
#7512=ORIENTED_EDGE ( 'NONE', *, *, #20585, .T. ) ;
#7528=DIRECTION ( 'NONE',  ( -0.9730401042858022320, 0.2306359803922080343, 5.959266323858941219E-17 ) ) ;
#7534=LINE ( 'NONE', #7421, #10536 ) ;
#7535=AXIS2_PLACEMENT_3D ( 'NONE', #2654, #6448, #13825 ) ;
#7536=CARTESIAN_POINT ( 'NONE',  ( 37.67179450110460692, -4.077824265976569329, -13.00000000000000000 ) ) ;
#7541=ADVANCED_FACE ( 'NONE', ( #2299 ), #4759, .F. ) ;
#7551=VERTEX_POINT ( 'NONE', #16903 ) ;
#7557=EDGE_LOOP ( 'NONE', ( #314, #5236, #20865, #9390 ) ) ;
#7558=CARTESIAN_POINT ( 'NONE',  ( 41.15130700480209924, 11.54075009235119964, 15.50000000000000000 ) ) ;
#7568=DIRECTION ( 'NONE',  ( -0.2306359803922053142, -0.9730401042858028982, 0.000000000000000000 ) ) ;
#7574=ADVANCED_FACE ( 'NONE', ( #2537 ), #15118, .T. ) ;
#7582=CARTESIAN_POINT ( 'NONE',  ( 62.31663085210120556, 16.28722946541822836, 3.908114637620867245E-14 ) ) ;
#7584=VECTOR ( 'NONE', #23389, 1000.000000000000114 ) ;
#7587=DIRECTION ( 'NONE',  ( 0.9730401042858024541, -0.2306359803922080898, -5.959266323858942451E-17 ) ) ;
#7603=EDGE_LOOP ( 'NONE', ( #13785, #9118, #12494, #20839 ) ) ;
#7609=VECTOR ( 'NONE', #19973, 1000.000000000000227 ) ;
#7611=ADVANCED_FACE ( 'NONE', ( #22005 ), #1059, .T. ) ;
#7615=CARTESIAN_POINT ( 'NONE',  ( 102.8131131701580046, 7.202356331284469171, -13.00000000000000000 ) ) ;
#7617=ORIENTED_EDGE ( 'NONE', *, *, #22186, .F. ) ;
#7618=CARTESIAN_POINT ( 'NONE',  ( 38.19845176233020823, -1.855887187839940777, -13.00000000000000000 ) ) ;
#7628=EDGE_LOOP ( 'NONE', ( #4847, #12910, #11490, #8549 ) ) ;
#7631=ORIENTED_EDGE ( 'NONE', *, *, #2134, .T. ) ;
#7634=CARTESIAN_POINT ( 'NONE',  ( 41.17437060284130013, 11.63805410277969976, -19.59999999999999787 ) ) ;
#7648=AXIS2_PLACEMENT_3D ( 'NONE', #10102, #22902, #13769 ) ;
#7652=CARTESIAN_POINT ( 'NONE',  ( 43.87899317387989839, 21.17128575569940097, 13.00000000000000000 ) ) ;
#7656=EDGE_CURVE ( 'NONE', #21726, #9182, #13235, .T. ) ;
#7675=AXIS2_PLACEMENT_3D ( 'NONE', #13561, #2278, #3954 ) ;
#7688=VERTEX_POINT ( 'NONE', #22921 ) ;
#7692=ORIENTED_EDGE ( 'NONE', *, *, #19736, .F. ) ;
#7703=VERTEX_POINT ( 'NONE', #17599 ) ;
#7707=VECTOR ( 'NONE', #7528, 1000.000000000000227 ) ;
#7710=CARTESIAN_POINT ( 'NONE',  ( 54.98564867634340203, -10.30593110903627441, 13.00000000000000000 ) ) ;
#7718=VERTEX_POINT ( 'NONE', #1304 ) ;
#7722=CARTESIAN_POINT ( 'NONE',  ( 114.8178196092480050, -22.36345201740219935, -13.00000000000000000 ) ) ;
#7739=AXIS2_PLACEMENT_3D ( 'NONE', #18889, #4393, #6290 ) ;
#7755=CARTESIAN_POINT ( 'NONE',  ( 114.1489752661110089, -25.18526831983109915, -3.000000000000000000 ) ) ;
#7757=ORIENTED_EDGE ( 'NONE', *, *, #18352, .F. ) ;
#7758=VERTEX_POINT ( 'NONE', #15692 ) ;
#7759=DIRECTION ( 'NONE',  ( 0.9730401042858024541, -0.2306359803922080898, -5.959266323853532591E-17 ) ) ;
#7766=CARTESIAN_POINT ( 'NONE',  ( 114.1489752661110089, -25.18526831983100323, -3.400000000000049649 ) ) ;
#7780=CARTESIAN_POINT ( 'NONE',  ( 35.84667945578129888, -10.83917230622230043, 3.100000000000039613 ) ) ;
#7784=AXIS2_PLACEMENT_3D ( 'NONE', #5023, #18287, #4903 ) ;
#7795=ADVANCED_FACE ( 'NONE', ( #10238, #4877, #21485, #14364, #8681, #5224 ), #17462, .T. ) ;
#7800=ORIENTED_EDGE ( 'NONE', *, *, #8995, .T. ) ;
#7807=VECTOR ( 'NONE', #4871, 1000.000000000000227 ) ;
#7808=CARTESIAN_POINT ( 'NONE',  ( 114.1489752661110089, -25.18526831983100323, 3.399999999999999911 ) ) ;
#7810=DIRECTION ( 'NONE',  ( 3.469446951953605354E-14, 9.757819552369514663E-14, -1.000000000000000000 ) ) ;
#7812=ORIENTED_EDGE ( 'NONE', *, *, #11599, .T. ) ;
#7815=ORIENTED_EDGE ( 'NONE', *, *, #12647, .F. ) ;
#7819=ORIENTED_EDGE ( 'NONE', *, *, #12479, .F. ) ;
#7830=EDGE_CURVE ( 'NONE', #8196, #19161, #16599, .T. ) ;
#7832=CONICAL_SURFACE ( 'NONE', #22613, 2.283500000000000085, 0.7853981633974447263 ) ;
#7834=AXIS2_PLACEMENT_3D ( 'NONE', #13770, #4623, #11769 ) ;
#7836=CARTESIAN_POINT ( 'NONE',  ( 113.8430260960419957, 8.210644904773758412, 3.037748485030009753E-14 ) ) ;
#7839=DIRECTION ( 'NONE',  ( 0.2306359803922080343, 0.9730401042858022320, -3.554125915991511201E-14 ) ) ;
#7847=ORIENTED_EDGE ( 'NONE', *, *, #15006, .T. ) ;
#7852=DIRECTION ( 'NONE',  ( 0.2306359803922076457, 0.9730401042858023430, -1.412237191019970710E-17 ) ) ;
#7853=AXIS2_PLACEMENT_3D ( 'NONE', #2725, #13643, #17224 ) ;
#7859=ORIENTED_EDGE ( 'NONE', *, *, #2811, .T. ) ;
#7862=LINE ( 'NONE', #11220, #8230 ) ;
#7865=DIRECTION ( 'NONE',  ( -0.2306359803922076457, -0.9730401042858024541, 1.412237191019896446E-17 ) ) ;
#7867=LINE ( 'NONE', #13333, #4652 ) ;
#7871=EDGE_CURVE ( 'NONE', #7718, #813, #5817, .T. ) ;
#7875=CARTESIAN_POINT ( 'NONE',  ( 41.17437060284130013, 11.63805410277969976, 20.00000000000000000 ) ) ;
#7890=FACE_OUTER_BOUND ( 'NONE', #2965, .T. ) ;
#7898=ORIENTED_EDGE ( 'NONE', *, *, #22094, .F. ) ;
#7904=EDGE_LOOP ( 'NONE', ( #338, #3688, #19908, #20763 ) ) ;
#7907=ORIENTED_EDGE ( 'NONE', *, *, #1811, .F. ) ;
#7919=DIRECTION ( 'NONE',  ( -0.9730401042858024541, 0.2306359803922080898, 5.959266323863172718E-17 ) ) ;
#7922=DIRECTION ( 'NONE',  ( 0.2306359803922053142, 0.9730401042858028982, 0.000000000000000000 ) ) ;
#7939=DIRECTION ( 'NONE',  ( 0.2306359803922080898, 0.9730401042858024541, -2.572202231434325988E-16 ) ) ;
#7941=EDGE_CURVE ( 'NONE', #11874, #19234, #8475, .T. ) ;
#7957=ADVANCED_FACE ( 'NONE', ( #11301 ), #16489, .F. ) ;
#7979=VECTOR ( 'NONE', #16675, 1000.000000000000227 ) ;
#7980=AXIS2_PLACEMENT_3D ( 'NONE', #17450, #20892, #10002 ) ;
#7981=CARTESIAN_POINT ( 'NONE',  ( 39.67523673029199927, 5.313293424922040487, -15.90000000000000036 ) ) ;
#7986=CIRCLE ( 'NONE', #6446, 2.066999999999999726 ) ;
#7989=LINE ( 'NONE', #1070, #19434 ) ;
#7996=ORIENTED_EDGE ( 'NONE', *, *, #12235, .F. ) ;
#8003=CARTESIAN_POINT ( 'NONE',  ( 114.1489752661110089, -25.18526831983100323, -3.400000000000049649 ) ) ;
#8006=DIRECTION ( 'NONE',  ( 0.2306359803922087282, 0.9730401042858021210, 2.478176394252581732E-15 ) ) ;
#8015=VECTOR ( 'NONE', #2219, 1000.000000000000227 ) ;
#8021=VERTEX_POINT ( 'NONE', #14486 ) ;
#8043=ORIENTED_EDGE ( 'NONE', *, *, #16314, .T. ) ;
#8058=CIRCLE ( 'NONE', #21321, 2.499999999999999112 ) ;
#8062=CARTESIAN_POINT ( 'NONE',  ( 39.67523673029199927, 5.313293424921989860, 18.89999999999999858 ) ) ;
#8065=VECTOR ( 'NONE', #6995, 1000.000000000000000 ) ;
#8073=ORIENTED_EDGE ( 'NONE', *, *, #12008, .T. ) ;
#8080=EDGE_CURVE ( 'NONE', #8503, #7688, #797, .T. ) ;
#8083=ADVANCED_FACE ( 'NONE', ( #8297 ), #13637, .F. ) ;
#8088=CARTESIAN_POINT ( 'NONE',  ( 117.1933702072879981, -12.34113894325840022, -19.59999999999999787 ) ) ;
#8104=AXIS2_PLACEMENT_3D ( 'NONE', #10037, #6690, #19164 ) ;
#8107=AXIS2_PLACEMENT_3D ( 'NONE', #5864, #20347, #4077 ) ;
#8108=ORIENTED_EDGE ( 'NONE', *, *, #1703, .F. ) ;
#8118=CYLINDRICAL_SURFACE ( 'NONE', #7675, 2.066999999999997950 ) ;
#8120=AXIS2_PLACEMENT_3D ( 'NONE', #13612, #7919, #4360 ) ;
#8128=LINE ( 'NONE', #8003, #10770 ) ;
#8146=EDGE_LOOP ( 'NONE', ( #611, #21373, #4111 ) ) ;
#8147=DIRECTION ( 'NONE',  ( 0.9730401042858024541, -0.2306359803922080898, -5.959266323858952312E-17 ) ) ;
#8148=DIRECTION ( 'NONE',  ( 1.000000000000000000, -6.124317834331790129E-17, 0.000000000000000000 ) ) ;
#8152=DIRECTION ( 'NONE',  ( -0.9730401042858023430, 0.2306359803922080620, 5.959266323858944916E-17 ) ) ;
#8159=ORIENTED_EDGE ( 'NONE', *, *, #6819, .T. ) ;
#8179=CARTESIAN_POINT ( 'NONE',  ( 43.40226860240920814, 19.16001186014064572, 13.00000000000000000 ) ) ;
#8180=EDGE_CURVE ( 'NONE', #4592, #6410, #22300, .T. ) ;
#8189=ORIENTED_EDGE ( 'NONE', *, *, #9317, .F. ) ;
#8196=VERTEX_POINT ( 'NONE', #15659 ) ;
#8213=ORIENTED_EDGE ( 'NONE', *, *, #18380, .T. ) ;
#8223=ADVANCED_FACE ( 'NONE', ( #17685 ), #8654, .T. ) ;
#8225=ORIENTED_EDGE ( 'NONE', *, *, #18352, .T. ) ;
#8230=VECTOR ( 'NONE', #16999, 1000.000000000000227 ) ;
#8233=PLANE ( 'NONE',  #8107 ) ;
#8238=DIRECTION ( 'NONE',  ( 0.000000000000000000, 0.000000000000000000, 1.000000000000000000 ) ) ;
#8240=EDGE_CURVE ( 'NONE', #563, #2422, #14161, .T. ) ;
#8260=ORIENTED_EDGE ( 'NONE', *, *, #8903, .T. ) ;
#8265=DIRECTION ( 'NONE',  ( 0.2306359803922094498, 0.9730401042858018990, 0.000000000000000000 ) ) ;
#8268=DIRECTION ( 'NONE',  ( 0.9730401042858024541, -0.2306359803922080898, -5.959266323858942451E-17 ) ) ;
#8270=EDGE_CURVE ( 'NONE', #16036, #14838, #6760, .T. ) ;
#8277=ORIENTED_EDGE ( 'NONE', *, *, #1696, .F. ) ;
#8282=ORIENTED_EDGE ( 'NONE', *, *, #2407, .F. ) ;
#8297=FACE_OUTER_BOUND ( 'NONE', #12044, .T. ) ;
#8298=ORIENTED_EDGE ( 'NONE', *, *, #12555, .F. ) ;
#8312=ORIENTED_EDGE ( 'NONE', *, *, #10326, .F. ) ;
#8314=ORIENTED_EDGE ( 'NONE', *, *, #17807, .T. ) ;
#8322=CARTESIAN_POINT ( 'NONE',  ( 46.93847685464109531, -4.150000499290836586, 13.00000000000000000 ) ) ;
#8323=EDGE_CURVE ( 'NONE', #19758, #8816, #5093, .T. ) ;
#8334=DIRECTION ( 'NONE',  ( 0.9730401042858024541, -0.2306359803922080898, -5.959266323859172946E-17 ) ) ;
#8338=EDGE_CURVE ( 'NONE', #14253, #9773, #1389, .T. ) ;
#8347=DIRECTION ( 'NONE',  ( 0.2306359803922053142, 0.9730401042858028982, 0.000000000000000000 ) ) ;
#8352=DIRECTION ( 'NONE',  ( -0.9730401042858024541, 0.2306359803922080898, 5.959266323858942451E-17 ) ) ;
#8369=AXIS2_PLACEMENT_3D ( 'NONE', #15374, #9814, #17032 ) ;
#8374=CARTESIAN_POINT ( 'NONE',  ( 39.83668191656649782, 5.994421497922140851, 18.89999999999999858 ) ) ;
#8377=VECTOR ( 'NONE', #9033, 1000.000000000000227 ) ;
#8378=DIRECTION ( 'NONE',  ( 2.676216343273230621E-30, -3.491853980617010126E-15, 1.000000000000000000 ) ) ;
#8379=VERTEX_POINT ( 'NONE', #17567 ) ;
#8382=CARTESIAN_POINT ( 'NONE',  ( 41.24356139695900225, 11.92996613406540085, 18.89999999999999858 ) ) ;
#8399=EDGE_CURVE ( 'NONE', #11037, #4401, #14802, .T. ) ;
#8406=ORIENTED_EDGE ( 'NONE', *, *, #4516, .T. ) ;
#8410=CARTESIAN_POINT ( 'NONE',  ( 118.5079952955230027, -6.794810348829390279, 15.90000000000000036 ) ) ;
#8441=CIRCLE ( 'NONE', #4258, 2.066999999999999726 ) ;
#8450=DIRECTION ( 'NONE',  ( -0.9730401042858024541, 0.2306359803922080898, 5.959266323858942451E-17 ) ) ;
#8462=CARTESIAN_POINT ( 'NONE',  ( 120.3930287342899987, 3.035456073538489896, 13.00000000000000000 ) ) ;
#8463=ORIENTED_EDGE ( 'NONE', *, *, #644, .F. ) ;
#8464=CARTESIAN_POINT ( 'NONE',  ( 37.46113131852679601, -4.027891576221660053, 13.00000000000000000 ) ) ;
#8467=ORIENTED_EDGE ( 'NONE', *, *, #20854, .F. ) ;
#8475=CIRCLE ( 'NONE', #16796, 2.066999999999998394 ) ;
#8477=EDGE_CURVE ( 'NONE', #23363, #14815, #23464, .T. ) ;
#8503=VERTEX_POINT ( 'NONE', #16569 ) ;
#8505=DIRECTION ( 'NONE',  ( -0.9730401042858024541, 0.2306359803922080898, 5.959266323858942451E-17 ) ) ;
#8508=EDGE_CURVE ( 'NONE', #11146, #17831, #9344, .T. ) ;
#8549=ORIENTED_EDGE ( 'NONE', *, *, #8338, .T. ) ;
#8554=CARTESIAN_POINT ( 'NONE',  ( 45.98502771169970060, -8.172548290408343519, -13.00000000000000000 ) ) ;
#8559=ORIENTED_EDGE ( 'NONE', *, *, #14630, .T. ) ;
#8564=VERTEX_POINT ( 'NONE', #11853 ) ;
#8565=CARTESIAN_POINT ( 'NONE',  ( 52.93501234483859719, 21.14904221214005631, 13.00000000000000000 ) ) ;
#8568=EDGE_CURVE ( 'NONE', #13613, #14838, #22270, .T. ) ;
#8571=EDGE_CURVE ( 'NONE', #13133, #1632, #4114, .T. ) ;
#8576=CARTESIAN_POINT ( 'NONE',  ( 39.67523673029199927, 5.313293424922060026, -18.89999999999999858 ) ) ;
#8578=CONICAL_SURFACE ( 'NONE', #21074, 2.283499999999998753, 0.7853981633974433940 ) ;
#8588=DIRECTION ( 'NONE',  ( 0.9730401042858024541, -0.2306359803922080898, -5.959266323858711956E-17 ) ) ;
#8608=VERTEX_POINT ( 'NONE', #18855 ) ;
#8611=EDGE_LOOP ( 'NONE', ( #6283, #23232, #5689, #15895 ) ) ;
#8652=CONICAL_SURFACE ( 'NONE', #21905, 1.033499999999999863, 1.029744258676650093 ) ;
#8654=PLANE ( 'NONE',  #2015 ) ;
#8657=ORIENTED_EDGE ( 'NONE', *, *, #20098, .F. ) ;
#8659=DIRECTION ( 'NONE',  ( 1.099672473571039977E-13, 0.000000000000000000, -1.000000000000000000 ) ) ;
#8681=FACE_BOUND ( 'NONE', #22556, .T. ) ;
#8696=EDGE_CURVE ( 'NONE', #1632, #21124, #18358, .T. ) ;
#8699=EDGE_CURVE ( 'NONE', #14649, #3226, #4471, .T. ) ;
#8701=DIRECTION ( 'NONE',  ( -0.9730401042858024541, 0.2306359803922080898, 5.959266323858942451E-17 ) ) ;
#8703=DIRECTION ( 'NONE',  ( -0.2306359803922083396, -0.9730401042858023430, 2.222614453595284847E-13 ) ) ;
#8705=LINE ( 'NONE', #13820, #13021 ) ;
#8706=DIRECTION ( 'NONE',  ( -0.2306359803922080343, -0.9730401042858022320, 3.554125915991511201E-14 ) ) ;
#8739=CARTESIAN_POINT ( 'NONE',  ( 37.14513723987899851, -6.299761344113198547, -13.00000000000000000 ) ) ;
#8775=VECTOR ( 'NONE', #22747, 1000.000000000000227 ) ;
#8781=VECTOR ( 'NONE', #18834, 1000.000000000000000 ) ;
#8807=EDGE_CURVE ( 'NONE', #11767, #8608, #21010, .T. ) ;
#8809=PLANE ( 'NONE',  #263 ) ;
#8812=ORIENTED_EDGE ( 'NONE', *, *, #7871, .T. ) ;
#8816=VERTEX_POINT ( 'NONE', #3034 ) ;
#8818=ORIENTED_EDGE ( 'NONE', *, *, #1526, .T. ) ;
#8829=AXIS2_PLACEMENT_3D ( 'NONE', #17728, #21159, #11941 ) ;
#8836=LINE ( 'NONE', #1686, #13213 ) ;
#8838=CONICAL_SURFACE ( 'NONE', #9216, 2.283500000000000085, 0.7853981633974469467 ) ;
#8840=CARTESIAN_POINT ( 'NONE',  ( 113.2956221386590130, -28.78551670568849730, 2.700000000000000178 ) ) ;
#8846=ORIENTED_EDGE ( 'NONE', *, *, #8568, .F. ) ;
#8850=CARTESIAN_POINT ( 'NONE',  ( 120.8697533057606961, 5.046729969097192736, -13.00000000000000000 ) ) ;
#8855=LINE ( 'NONE', #12412, #842 ) ;
#8869=VECTOR ( 'NONE', #14456, 1000.000000000000000 ) ;
#8874=DIRECTION ( 'NONE',  ( -0.9730401042858024541, 0.2306359803922080898, 5.959266323858942451E-17 ) ) ;
#8877=CARTESIAN_POINT ( 'NONE',  ( 114.8732178155626826, -20.25231274233364687, 13.00000000000000000 ) ) ;
#8883=CARTESIAN_POINT ( 'NONE',  ( 118.5079952955230027, -6.794810348829379620, -15.90000000000000036 ) ) ;
#8884=EDGE_LOOP ( 'NONE', ( #20548, #20449, #16984 ) ) ;
#8885=CONICAL_SURFACE ( 'NONE', #18294, 2.283499999999998753, 0.7853981633974433940 ) ;
#8888=DIRECTION ( 'NONE',  ( -0.9730401042858022320, 0.2306359803922080343, 5.959266323858941219E-17 ) ) ;
#8890=DIRECTION ( 'NONE',  ( -4.328311834315510110E-15, -1.851928590941880236E-14, 1.000000000000000000 ) ) ;
#8892=CIRCLE ( 'NONE', #7739, 2.066999999999998394 ) ;
#8896=DIRECTION ( 'NONE',  ( 0.2306359803922080898, 0.9730401042858024541, -2.572202231434325988E-16 ) ) ;
#8901=FACE_OUTER_BOUND ( 'NONE', #7441, .T. ) ;
#8903=EDGE_CURVE ( 'NONE', #12330, #12414, #5519, .T. ) ;
#8920=DIRECTION ( 'NONE',  ( -0.2306359803922053142, -0.9730401042858028982, 0.000000000000000000 ) ) ;
#8929=DIRECTION ( 'NONE',  ( 0.2306359803922085339, 0.9730401042858022320, 0.000000000000000000 ) ) ;
#8940=CARTESIAN_POINT ( 'NONE',  ( 114.2412296582679971, -24.79605227811680379, 3.000000000000000000 ) ) ;
#8954=LINE ( 'NONE', #10984, #14513 ) ;
#8963=PLANE ( 'NONE',  #17188 ) ;
#8969=LINE ( 'NONE', #1468, #6744 ) ;
#8971=FACE_OUTER_BOUND ( 'NONE', #23123, .T. ) ;
#8993=ORIENTED_EDGE ( 'NONE', *, *, #19519, .T. ) ;
#8995=EDGE_CURVE ( 'NONE', #12330, #19270, #12539, .T. ) ;
#9004=ORIENTED_EDGE ( 'NONE', *, *, #14345, .T. ) ;
#9006=AXIS2_PLACEMENT_3D ( 'NONE', #22825, #20931, #20590 ) ;
#9007=VECTOR ( 'NONE', #5342, 1000.000000000000000 ) ;
#9015=AXIS2_PLACEMENT_3D ( 'NONE', #973, #15587, #11947 ) ;
#9027=LINE ( 'NONE', #16258, #1707 ) ;
#9033=DIRECTION ( 'NONE',  ( -0.2306359803922080343, -0.9730401042858022320, 5.076717492620541185E-14 ) ) ;
#9036=DIRECTION ( 'NONE',  ( 0.2306359803922080343, 0.9730401042858022320, -2.572202231434325495E-16 ) ) ;
#9039=ORIENTED_EDGE ( 'NONE', *, *, #23080, .F. ) ;
#9047=DIRECTION ( 'NONE',  ( 0.1187863113461967018, 0.5011527021216418687, 0.8571673007021100021 ) ) ;
#9049=CARTESIAN_POINT ( 'NONE',  ( 114.9405074087380001, 12.84085624101770051, -2.283499999999970775 ) ) ;
#9050=CARTESIAN_POINT ( 'NONE',  ( 83.72351314638889619, 11.21323789678963934, 3.777010778495970333E-14 ) ) ;
#9054=VERTEX_POINT ( 'NONE', #20709 ) ;
#9059=ADVANCED_FACE ( 'NONE', ( #7890 ), #11242, .F. ) ;
#9065=DIRECTION ( 'NONE',  ( -0.9730401042858024541, 0.2306359803922080898, 5.959266323858942451E-17 ) ) ;
#9092=CARTESIAN_POINT ( 'NONE',  ( 53.15246078658950069, 27.48624099592299785, 3.293763653412249631E-14 ) ) ;
#9093=ORIENTED_EDGE ( 'NONE', *, *, #11317, .F. ) ;
#9095=ORIENTED_EDGE ( 'NONE', *, *, #833, .T. ) ;
#9097=CARTESIAN_POINT ( 'NONE',  ( 111.8137341348020044, 5.068973512656589797, 13.00000000000000000 ) ) ;
#9098=ORIENTED_EDGE ( 'NONE', *, *, #20000, .T. ) ;
#9100=DIRECTION ( 'NONE',  ( -0.9730401042858024541, 0.2306359803922080898, 5.959266323859082967E-17 ) ) ;
#9108=VECTOR ( 'NONE', #21532, 1000.000000000000000 ) ;
#9114=FACE_OUTER_BOUND ( 'NONE', #19370, .T. ) ;
#9118=ORIENTED_EDGE ( 'NONE', *, *, #12647, .T. ) ;
#9148=DIRECTION ( 'NONE',  ( -0.2306359803922085339, -0.9730401042858022320, 0.000000000000000000 ) ) ;
#9153=CARTESIAN_POINT ( 'NONE',  ( 43.45766680872420551, 21.27115113520920175, -20.00000000000000000 ) ) ;
#9171=MANIFOLD_SOLID_BREP ( 'Imported1', #17788 ) ;
#9175=LINE ( 'NONE', #19747, #9492 ) ;
#9177=CARTESIAN_POINT ( 'NONE',  ( 36.79228697538940196, -6.849707878650439952, 3.399999999999999911 ) ) ;
#9180=CARTESIAN_POINT ( 'NONE',  ( 96.81657767996070163, -18.09668638014640152, 13.00000000000000000 ) ) ;
#9182=VERTEX_POINT ( 'NONE', #14799 ) ;
#9188=DIRECTION ( 'NONE',  ( -0.9730401042858022320, 0.2306359803922080343, 5.959266323858941219E-17 ) ) ;
#9192=ORIENTED_EDGE ( 'NONE', *, *, #4262, .F. ) ;
#9206=CARTESIAN_POINT ( 'NONE',  ( 37.40573311221180575, -6.139030851290243618, -13.00000000000000000 ) ) ;
#9213=ORIENTED_EDGE ( 'NONE', *, *, #2134, .F. ) ;
#9216=AXIS2_PLACEMENT_3D ( 'NONE', #20023, #22146, #3746 ) ;
#9237=VECTOR ( 'NONE', #1555, 1000.000000000000000 ) ;
#9248=VECTOR ( 'NONE', #9951, 1000.000000000000227 ) ;
#9261=ADVANCED_FACE ( 'NONE', ( #15721 ), #17077, .F. ) ;
#9268=ORIENTED_EDGE ( 'NONE', *, *, #23114, .F. ) ;
#9282=ORIENTED_EDGE ( 'NONE', *, *, #1057, .T. ) ;
#9289=ORIENTED_EDGE ( 'NONE', *, *, #1038, .T. ) ;
#9309=DIRECTION ( 'NONE',  ( -0.2306359803922094498, -0.9730401042858020100, 1.412237191019847142E-17 ) ) ;
#9311=AXIS2_PLACEMENT_3D ( 'NONE', #16118, #5539, #18027 ) ;
#9314=DIRECTION ( 'NONE',  ( 0.000000000000000000, 0.000000000000000000, -1.000000000000000000 ) ) ;
#9317=EDGE_CURVE ( 'NONE', #23097, #21550, #7986, .T. ) ;
#9336=DIRECTION ( 'NONE',  ( 0.9730401042858024541, -0.2306359803922080898, -5.959266323858942451E-17 ) ) ;
#9342=AXIS2_PLACEMENT_3D ( 'NONE', #15556, #4757, #6064 ) ;
#9344=LINE ( 'NONE', #299, #8869 ) ;
#9348=ORIENTED_EDGE ( 'NONE', *, *, #20530, .T. ) ;
#9371=FACE_OUTER_BOUND ( 'NONE', #4153, .T. ) ;
#9372=EDGE_CURVE ( 'NONE', #15812, #22407, #11406, .T. ) ;
#9382=ORIENTED_EDGE ( 'NONE', *, *, #2394, .F. ) ;
#9385=LINE ( 'NONE', #4277, #1026 ) ;
#9390=ORIENTED_EDGE ( 'NONE', *, *, #2389, .T. ) ;
#9400=CIRCLE ( 'NONE', #22259, 2.066999999999999726 ) ;
#9412=EDGE_CURVE ( 'NONE', #171, #10848, #14276, .T. ) ;
#9417=EDGE_CURVE ( 'NONE', #12312, #20142, #5494, .T. ) ;
#9419=DIRECTION ( 'NONE',  ( -0.9730401042858024541, 0.2306359803922080898, 5.959266323858942451E-17 ) ) ;
#9422=ORIENTED_EDGE ( 'NONE', *, *, #8807, .T. ) ;
#9423=FACE_OUTER_BOUND ( 'NONE', #12115, .T. ) ;
#9431=LINE ( 'NONE', #14882, #18348 ) ;
#9436=CARTESIAN_POINT ( 'NONE',  ( 61.45890873801150178, 17.00438549795330090, -13.00000000000000000 ) ) ;
#9441=DIRECTION ( 'NONE',  ( 0.2306359803922095053, 0.9730401042858018990, 0.000000000000000000 ) ) ;
#9446=FACE_OUTER_BOUND ( 'NONE', #7378, .T. ) ;
#9452=DIRECTION ( 'NONE',  ( 9.912705577010324563E-16, 2.478176394252581338E-15, -1.000000000000000000 ) ) ;
#9458=DIRECTION ( 'NONE',  ( -0.2306359803922085339, -0.9730401042858022320, 0.000000000000000000 ) ) ;
#9466=AXIS2_PLACEMENT_3D ( 'NONE', #17864, #8505, #19185 ) ;
#9467=ORIENTED_EDGE ( 'NONE', *, *, #14220, .F. ) ;
#9469=CYLINDRICAL_SURFACE ( 'NONE', #18620, 2.066999999999998394 ) ;
#9478=EDGE_CURVE ( 'NONE', #2422, #9929, #9175, .T. ) ;
#9492=VECTOR ( 'NONE', #10868, 1000.000000000000227 ) ;
#9500=CYLINDRICAL_SURFACE ( 'NONE', #2718, 2.066999999999999726 ) ;
#9501=ORIENTED_EDGE ( 'NONE', *, *, #22676, .T. ) ;
#9502=CIRCLE ( 'NONE', #8369, 2.500000000000000000 ) ;
#9504=CARTESIAN_POINT ( 'NONE',  ( 118.6002496876800052, -6.405594307115060282, 15.90000000000000036 ) ) ;
#9510=VECTOR ( 'NONE', #20503, 1000.000000000000227 ) ;
#9538=FACE_OUTER_BOUND ( 'NONE', #3585, .T. ) ;
#9542=CYLINDRICAL_SURFACE ( 'NONE', #5775, 0.3999999999999982458 ) ;
#9553=FACE_OUTER_BOUND ( 'NONE', #4620, .T. ) ;
#9556=FACE_OUTER_BOUND ( 'NONE', #15884, .T. ) ;
#9561=DIRECTION ( 'NONE',  ( 0.2306359803922085339, 0.9730401042858022320, 0.000000000000000000 ) ) ;
#9603=CARTESIAN_POINT ( 'NONE',  ( 114.8178196092480050, -22.36345201740219935, -13.00000000000000000 ) ) ;
#9613=VERTEX_POINT ( 'NONE', #14749 ) ;
#9617=CARTESIAN_POINT ( 'NONE',  ( 117.1241794131703529, -12.63305097454429848, 3.419367484756719403E-14 ) ) ;
#9626=CIRCLE ( 'NONE', #20219, 2.066999999999998394 ) ;
#9631=VECTOR ( 'NONE', #5515, 1000.000000000000227 ) ;
#9648=VERTEX_POINT ( 'NONE', #15217 ) ;
#9656=VECTOR ( 'NONE', #7427, 1000.000000000000227 ) ;
#9676=VERTEX_POINT ( 'NONE', #4175 ) ;
#9677=ORIENTED_EDGE ( 'NONE', *, *, #21118, .T. ) ;
#9682=DIRECTION ( 'NONE',  ( -0.9730401042858024541, 0.2306359803922080898, 5.959266323858942451E-17 ) ) ;
#9685=CARTESIAN_POINT ( 'NONE',  ( 35.84667945578129888, -10.83917230622219918, 13.00000000000000000 ) ) ;
#9690=CARTESIAN_POINT ( 'NONE',  ( 43.45766680872420551, 21.27115113520920175, -20.00000000000000000 ) ) ;
#9696=CARTESIAN_POINT ( 'NONE',  ( 36.10037903421270755, -9.768828191507928693, -2.700000000000000178 ) ) ;
#9706=DIRECTION ( 'NONE',  ( -0.9730401042858024541, 0.2306359803922080898, 5.959266323858942451E-17 ) ) ;
#9709=CARTESIAN_POINT ( 'NONE',  ( 114.8178196092480050, -22.36345201740209987, 20.00000000000000000 ) ) ;
#9718=VERTEX_POINT ( 'NONE', #16878 ) ;
#9729=EDGE_CURVE ( 'NONE', #15201, #171, #18562, .T. ) ;
#9731=EDGE_CURVE ( 'NONE', #16103, #11767, #17603, .T. ) ;
#9743=DIRECTION ( 'NONE',  ( -0.2306359803922094498, -0.9730401042858020100, 1.412237191019847142E-17 ) ) ;
#9745=DIRECTION ( 'NONE',  ( 1.302733484953870109E-15, 5.237774525740650345E-15, 1.000000000000000000 ) ) ;
#9750=CIRCLE ( 'NONE', #2528, 2.066999999999997506 ) ;
#9758=ORIENTED_EDGE ( 'NONE', *, *, #9412, .T. ) ;
#9762=ORIENTED_EDGE ( 'NONE', *, *, #3740, .F. ) ;
#9769=AXIS2_PLACEMENT_3D ( 'NONE', #13880, #5314, #19465 ) ;
#9770=VECTOR ( 'NONE', #19287, 1000.000000000000000 ) ;
#9773=VERTEX_POINT ( 'NONE', #10367 ) ;
#9776=CARTESIAN_POINT ( 'NONE',  ( 39.76749112244890227, 5.702509466636369595, -15.50000000000000000 ) ) ;
#9780=DIRECTION ( 'NONE',  ( 0.2306359803922085339, 0.9730401042858022320, 0.000000000000000000 ) ) ;
#9791=LINE ( 'NONE', #20699, #3166 ) ;
#9795=CARTESIAN_POINT ( 'NONE',  ( 55.46237324781409939, -8.294657213477510282, -13.00000000000000000 ) ) ;
#9797=CIRCLE ( 'NONE', #23041, 2.066999999999998394 ) ;
#9812=CARTESIAN_POINT ( 'NONE',  ( 59.43368109719860826, 4.124228161845699958, 3.772686752615189359E-14 ) ) ;
#9814=DIRECTION ( 'NONE',  ( 0.2306359803922080898, 0.9730401042858024541, -2.572202231434325988E-16 ) ) ;
#9818=DIRECTION ( 'NONE',  ( -0.9730401042858022320, 0.2306359803922080343, 5.959266323858941219E-17 ) ) ;
#9820=FACE_OUTER_BOUND ( 'NONE', #463, .T. ) ;
#9825=DIRECTION ( 'NONE',  ( 0.2306359803921919083, 0.9730401042858062288, 8.673617379884073337E-14 ) ) ;
#9831=ORIENTED_EDGE ( 'NONE', *, *, #22234, .F. ) ;
#9833=FACE_OUTER_BOUND ( 'NONE', #14914, .T. ) ;
#9834=VERTEX_POINT ( 'NONE', #2753 ) ;
#9835=DIRECTION ( 'NONE',  ( 2.561207961876604989E-14, 0.000000000000000000, -1.000000000000000000 ) ) ;
#9837=VERTEX_POINT ( 'NONE', #4997 ) ;
#9852=CIRCLE ( 'NONE', #1480, 2.499999999999999112 ) ;
#9866=ORIENTED_EDGE ( 'NONE', *, *, #5781, .F. ) ;
#9897=APPLICATION_CONTEXT ( 'configuration controlled 3d designs of mechanical parts and assemblies' ) ;
#9909=DIRECTION ( 'NONE',  ( -0.9730401042858022320, 0.2306359803922080343, 5.959266323858941219E-17 ) ) ;
#9919=LINE ( 'NONE', #11359, #4474 ) ;
#9923=LINE ( 'NONE', #6345, #13321 ) ;
#9928=AXIS2_PLACEMENT_3D ( 'NONE', #6985, #20980, #10195 ) ;
#9929=VERTEX_POINT ( 'NONE', #14251 ) ;
#9936=ADVANCED_FACE ( 'NONE', ( #17715 ), #9469, .F. ) ;
#9940=PLANE ( 'NONE',  #2263 ) ;
#9944=CARTESIAN_POINT ( 'NONE',  ( 114.8178196092480050, -22.36345201740209987, 20.00000000000000000 ) ) ;
#9951=DIRECTION ( 'NONE',  ( -0.9730401042858022320, 0.2306359803922080343, 5.959266323858941219E-17 ) ) ;
#9954=EDGE_CURVE ( 'NONE', #1222, #2277, #15960, .T. ) ;
#9957=CARTESIAN_POINT ( 'NONE',  ( 117.0319250210129951, -13.02226701625849969, -18.89999999999999858 ) ) ;
#9974=VECTOR ( 'NONE', #16985, 1000.000000000000227 ) ;
#9980=DIRECTION ( 'NONE',  ( 0.2306359803922076457, 0.9730401042858023430, 0.000000000000000000 ) ) ;
#9985=EDGE_LOOP ( 'NONE', ( #18452, #12188, #3542, #7494 ) ) ;
#10002=DIRECTION ( 'NONE',  ( 0.2306359803922053142, 0.9730401042858028982, 0.000000000000000000 ) ) ;
#10006=EDGE_CURVE ( 'NONE', #300, #14758, #23273, .T. ) ;
#10009=AXIS2_PLACEMENT_3D ( 'NONE', #15584, #4783, #12736 ) ;
#10010=ORIENTED_EDGE ( 'NONE', *, *, #6305, .F. ) ;
#10027=DIRECTION ( 'NONE',  ( 1.085472681297010170E-15, 4.321163532573060300E-15, 1.000000000000000000 ) ) ;
#10037=CARTESIAN_POINT ( 'NONE',  ( 117.0319250210129951, -13.02226701625859917, 15.90000000000000036 ) ) ;
#10042=FACE_BOUND ( 'NONE', #13365, .T. ) ;
#10046=DIRECTION ( 'NONE',  ( 0.5249589903860194529, -0.8511275218278935295, 5.444325428271645316E-17 ) ) ;
#10050=VECTOR ( 'NONE', #3306, 1000.000000000000000 ) ;
#10051=CARTESIAN_POINT ( 'NONE',  ( 122.4288069621910040, 9.746871424029301068, 13.00000000000000000 ) ) ;
#10064=CARTESIAN_POINT ( 'NONE',  ( 114.1489752661110089, -25.18526831983109915, 3.000000000000000000 ) ) ;
#10075=AXIS2_PLACEMENT_3D ( 'NONE', #570, #15174, #22537 ) ;
#10101=EDGE_LOOP ( 'NONE', ( #22992, #3460 ) ) ;
#10102=CARTESIAN_POINT ( 'NONE',  ( 114.8178196092480050, -22.36345201740219935, -13.00000000000000000 ) ) ;
#10103=FACE_OUTER_BOUND ( 'NONE', #21128, .T. ) ;
#10118=EDGE_CURVE ( 'NONE', #11037, #11043, #13503, .T. ) ;
#10137=CARTESIAN_POINT ( 'NONE',  ( 117.1933702072879981, -12.34113894325849969, 19.59999999999999787 ) ) ;
#10139=AXIS2_PLACEMENT_3D ( 'NONE', #17527, #8268, #11844 ) ;
#10149=ADVANCED_FACE ( 'NONE', ( #9833 ), #11518, .F. ) ;
#10151=DIRECTION ( 'NONE',  ( -0.2306359803922080620, -0.9730401042858023430, -1.901827233595000632E-14 ) ) ;
#10155=EDGE_CURVE ( 'NONE', #19234, #11874, #20131, .T. ) ;
#10162=CARTESIAN_POINT ( 'NONE',  ( 118.6002496876800052, -6.405594307115080710, -18.89999999999999858 ) ) ;
#10173=EDGE_LOOP ( 'NONE', ( #6270, #17918, #15057, #2881 ) ) ;
#10188=EDGE_CURVE ( 'NONE', #9834, #14253, #1007, .T. ) ;
#10195=DIRECTION ( 'NONE',  ( -0.9730401042858022320, 0.2306359803922080343, 1.051187380996432105E-30 ) ) ;
#10219=EDGE_CURVE ( 'NONE', #9718, #11739, #4590, .T. ) ;
#10221=LINE ( 'NONE', #582, #3569 ) ;
#10224=ORIENTED_EDGE ( 'NONE', *, *, #11010, .T. ) ;
#10225=CARTESIAN_POINT ( 'NONE',  ( 41.17437060284130013, 11.63805410277969976, 20.00000000000000000 ) ) ;
#10226=ORIENTED_EDGE ( 'NONE', *, *, #12770, .T. ) ;
#10236=CARTESIAN_POINT ( 'NONE',  ( 48.79336017845105999, 1.507728449240719915, 3.776618445270551233E-14 ) ) ;
#10238=FACE_BOUND ( 'NONE', #13887, .T. ) ;
#10265=ADVANCED_FACE ( 'NONE', ( #12430 ), #3384, .F. ) ;
#10271=VECTOR ( 'NONE', #14524, 1000.000000000000000 ) ;
#10274=CARTESIAN_POINT ( 'NONE',  ( 37.67179450110460692, -4.077824265976569329, 13.00000000000000000 ) ) ;
#10275=CARTESIAN_POINT ( 'NONE',  ( 120.8143550994449953, 2.935590694028629599, 20.00000000000000000 ) ) ;
#10282=ORIENTED_EDGE ( 'NONE', *, *, #8338, .F. ) ;
#10286=LINE ( 'NONE', #1106, #2757 ) ;
#10294=CARTESIAN_POINT ( 'NONE',  ( 122.7747609327790030, 11.20643158045800014, 9.133960000000000079 ) ) ;
#10296=DIRECTION ( 'NONE',  ( 0.2306359803922080343, 0.9730401042858022320, -1.015202274805050187E-13 ) ) ;
#10321=AXIS2_PLACEMENT_3D ( 'NONE', #3651, #19577, #16125 ) ;
#10326=EDGE_CURVE ( 'NONE', #503, #3857, #1879, .T. ) ;
#10327=DIRECTION ( 'NONE',  ( -0.9730401042858022320, 0.2306359803922080343, 5.959266323858941219E-17 ) ) ;
#10334=EDGE_LOOP ( 'NONE', ( #4352, #17605, #16132, #1871 ) ) ;
#10336=AXIS2_PLACEMENT_3D ( 'NONE', #18738, #6007, #20144 ) ;
#10342=LINE ( 'NONE', #4975, #10050 ) ;
#10345=VERTEX_POINT ( 'NONE', #8877 ) ;
#10367=CARTESIAN_POINT ( 'NONE',  ( 43.45766680872420551, 21.27115113520920175, 20.00000000000000000 ) ) ;
#10369=CARTESIAN_POINT ( 'NONE',  ( 122.4288069621910040, 9.746871424029221131, -10.02499999999999858 ) ) ;
#10371=VECTOR ( 'NONE', #16808, 1000.000000000000227 ) ;
#10378=DIRECTION ( 'NONE',  ( -0.9730401042858024541, 0.2306359803922080898, 5.959266323858942451E-17 ) ) ;
#10380=ORIENTED_EDGE ( 'NONE', *, *, #16218, .T. ) ;
#10382=LINE ( 'NONE', #1198, #17585 ) ;
#10394=ADVANCED_FACE ( 'NONE', ( #2926 ), #15863, .T. ) ;
#10395=CIRCLE ( 'NONE', #487, 0.4000000000000010214 ) ;
#10412=AXIS2_PLACEMENT_3D ( 'NONE', #23096, #1485, #15641 ) ;
#10418=ORIENTED_EDGE ( 'NONE', *, *, #21250, .F. ) ;
#10425=AXIS2_PLACEMENT_3D ( 'NONE', #6926, #5003, #6913 ) ;
#10458=ORIENTED_EDGE ( 'NONE', *, *, #1857, .F. ) ;
#10463=CARTESIAN_POINT ( 'NONE',  ( 113.4570673249340018, -28.10438863268850085, 2.700000000000049916 ) ) ;
#10473=AXIS2_PLACEMENT_3D ( 'NONE', #3187, #17563, #9980 ) ;
#10474=ORIENTED_EDGE ( 'NONE', *, *, #10188, .F. ) ;
#10478=CARTESIAN_POINT ( 'NONE',  ( 40.32424593841290061, 8.051426419082240216, -1.980584223082610025E-14 ) ) ;
#10497=CARTESIAN_POINT ( 'NONE',  ( 46.46175228317039796, -6.161274394849590053, 13.00000000000000000 ) ) ;
#10501=LINE ( 'NONE', #19621, #14807 ) ;
#10504=EDGE_LOOP ( 'NONE', ( #12951, #5104, #18616, #19917 ) ) ;
#10505=DIRECTION ( 'NONE',  ( -6.124317834331790129E-17, 2.578073951808930140E-21, -1.000000000000000000 ) ) ;
#10523=CARTESIAN_POINT ( 'NONE',  ( 113.2956221386590130, -28.78551670568859677, -3.100000000000000089 ) ) ;
#10525=EDGE_LOOP ( 'NONE', ( #21328, #7898, #12656, #9348 ) ) ;
#10527=CIRCLE ( 'NONE', #6738, 0.3999999999999998557 ) ;
#10536=VECTOR ( 'NONE', #3964, 1000.000000000000227 ) ;
#10556=ORIENTED_EDGE ( 'NONE', *, *, #11595, .F. ) ;
#10566=CARTESIAN_POINT ( 'NONE',  ( 122.7747609327790030, 11.20643158045800014, -9.133960000000000079 ) ) ;
#10570=CARTESIAN_POINT ( 'NONE',  ( 117.1241794131700118, -12.63305097454420078, -15.50000000000000000 ) ) ;
#10571=ORIENTED_EDGE ( 'NONE', *, *, #8080, .F. ) ;
#10573=LINE ( 'NONE', #23472, #13337 ) ;
#10581=ORIENTED_EDGE ( 'NONE', *, *, #9317, .T. ) ;
#10583=VERTEX_POINT ( 'NONE', #7780 ) ;
#10601=CARTESIAN_POINT ( 'NONE',  ( 122.4288069621910040, 9.746871424029221131, -10.02499999999999858 ) ) ;
#10603=CARTESIAN_POINT ( 'NONE',  ( 118.4388045014059969, -7.086722380115170417, -18.89999999999999858 ) ) ;
#10605=EDGE_LOOP ( 'NONE', ( #3512, #2250, #19951, #23049 ) ) ;
#10622=DIRECTION ( 'NONE',  ( -0.9730401042858024541, 0.2306359803922080898, 5.959266323858952312E-17 ) ) ;
#10639=AXIS2_PLACEMENT_3D ( 'NONE', #1667, #1895, #8929 ) ;
#10640=DIRECTION ( 'NONE',  ( -1.000000000000000000, 0.000000000000000000, -1.749697687229200179E-14 ) ) ;
#10641=ORIENTED_EDGE ( 'NONE', *, *, #12359, .T. ) ;
#10648=CYLINDRICAL_SURFACE ( 'NONE', #21151, 2.066999999999999726 ) ;
#10661=EDGE_CURVE ( 'NONE', #14490, #1632, #9923, .T. ) ;
#10693=CARTESIAN_POINT ( 'NONE',  ( 43.87899317387989839, 21.17128575569940097, 13.00000000000000000 ) ) ;
#10717=ORIENTED_EDGE ( 'NONE', *, *, #752, .F. ) ;
#10718=EDGE_CURVE ( 'NONE', #19011, #21767, #11362, .T. ) ;
#10723=CARTESIAN_POINT ( 'NONE',  ( 39.67523673029199927, 5.313293424921989860, 18.89999999999999858 ) ) ;
#10726=CYLINDRICAL_SURFACE ( 'NONE', #10639, 2.066999999999999726 ) ;
#10730=ORIENTED_EDGE ( 'NONE', *, *, #17072, .T. ) ;
#10733=AXIS2_PLACEMENT_3D ( 'NONE', #22877, #15637, #6740 ) ;
#10738=DIRECTION ( 'NONE',  ( 0.2306359803922080898, 0.9730401042858024541, -2.572202231434325988E-16 ) ) ;
#10746=PLANE ( 'NONE',  #15098 ) ;
#10756=FACE_OUTER_BOUND ( 'NONE', #8884, .T. ) ;
#10759=CARTESIAN_POINT ( 'NONE',  ( 112.6956120935907251, 3.369770385951719849, 2.067000000000031701 ) ) ;
#10760=VECTOR ( 'NONE', #207, 1000.000000000000227 ) ;
#10768=FACE_OUTER_BOUND ( 'NONE', #2055, .T. ) ;
#10770=VECTOR ( 'NONE', #9909, 1000.000000000000227 ) ;
#10773=FACE_OUTER_BOUND ( 'NONE', #17667, .T. ) ;
#10777=DIRECTION ( 'NONE',  ( -0.9730401042858024541, 0.2306359803922080898, 5.959266323858723049E-17 ) ) ;
#10780=EDGE_CURVE ( 'NONE', #813, #10964, #19633, .T. ) ;
#10790=CARTESIAN_POINT ( 'NONE',  ( 105.1303954406765939, 6.139246328161051203, 3.645906919371072791E-14 ) ) ;
#10795=DIRECTION ( 'NONE',  ( 0.000000000000000000, 0.000000000000000000, -1.000000000000000000 ) ) ;
#10803=CARTESIAN_POINT ( 'NONE',  ( 122.7747609327790030, 11.20643158045800014, -9.133960000000000079 ) ) ;
#10806=DIRECTION ( 'NONE',  ( 1.000000000000000000, -5.913983195221379736E-15, 0.000000000000000000 ) ) ;
#10811=ORIENTED_EDGE ( 'NONE', *, *, #17901, .T. ) ;
#10814=ORIENTED_EDGE ( 'NONE', *, *, #11446, .T. ) ;
#10828=CIRCLE ( 'NONE', #6649, 0.3999999999999982458 ) ;
#10829=DIRECTION ( 'NONE',  ( -0.9730401042858024541, 0.2306359803922080898, 5.959266323858942451E-17 ) ) ;
#10844=DIRECTION ( 'NONE',  ( -0.9730401042858024541, 0.2306359803922080898, 5.959266323858942451E-17 ) ) ;
#10848=VERTEX_POINT ( 'NONE', #12402 ) ;
#10853=LINE ( 'NONE', #7161, #984 ) ;
#10858=EDGE_CURVE ( 'NONE', #23458, #9773, #16959, .T. ) ;
#10868=DIRECTION ( 'NONE',  ( 0.2306359803922080343, 0.9730401042858022320, -2.572202231434325495E-16 ) ) ;
#10871=DIRECTION ( 'NONE',  ( -0.9730401042858022320, 0.2306359803922080343, 5.959266323858941219E-17 ) ) ;
#10872=DIRECTION ( 'NONE',  ( 0.2306359803922080898, 0.9730401042858024541, -2.572202231434325988E-16 ) ) ;
#10875=EDGE_CURVE ( 'NONE', #19270, #2029, #15724, .T. ) ;
#10877=CARTESIAN_POINT ( 'NONE',  ( 117.0319250210129951, -13.02226701625859917, 18.89999999999999858 ) ) ;
#10883=ORIENTED_EDGE ( 'NONE', *, *, #8323, .F. ) ;
#10897=CARTESIAN_POINT ( 'NONE',  ( 118.6002496876800052, -6.405594307115080710, -18.89999999999999858 ) ) ;
#10912=AXIS2_PLACEMENT_3D ( 'NONE', #21116, #19578, #7011 ) ;
#10914=EDGE_CURVE ( 'NONE', #19758, #8608, #18331, .T. ) ;
#10919=VECTOR ( 'NONE', #10871, 1000.000000000000227 ) ;
#10938=AXIS2_PLACEMENT_3D ( 'NONE', #19495, #23039, #4528 ) ;
#10945=VECTOR ( 'NONE', #20376, 1000.000000000000227 ) ;
#10955=VECTOR ( 'NONE', #2150, 1000.000000000000000 ) ;
#10959=LINE ( 'NONE', #9153, #4925 ) ;
#10964=VERTEX_POINT ( 'NONE', #21870 ) ;
#10969=DIRECTION ( 'NONE',  ( 0.000000000000000000, 0.000000000000000000, 1.000000000000000000 ) ) ;
#10970=DIRECTION ( 'NONE',  ( 0.1187863113461966047, 0.5011527021216413136, -0.8571673007021102242 ) ) ;
#10978=DIRECTION ( 'NONE',  ( 0.2306359803922080343, 0.9730401042858022320, 5.907067092757111157E-15 ) ) ;
#10984=CARTESIAN_POINT ( 'NONE',  ( 113.2033677465029911, -29.17473274740279976, -13.00000000000000000 ) ) ;
#10991=DIRECTION ( 'NONE',  ( -0.9730401042858022320, 0.2306359803922080343, 5.959266323858941219E-17 ) ) ;
#10997=AXIS2_PLACEMENT_3D ( 'NONE', #14291, #15733, #4697 ) ;
#10998=DIRECTION ( 'NONE',  ( 2.853725266239763049E-28, 3.456932630710235087E-14, 1.000000000000000000 ) ) ;
#11001=EDGE_CURVE ( 'NONE', #5106, #9182, #4436, .T. ) ;
#11009=EDGE_CURVE ( 'NONE', #13082, #14490, #10527, .T. ) ;
#11010=EDGE_CURVE ( 'NONE', #12312, #4592, #19997, .T. ) ;
#11014=LINE ( 'NONE', #18370, #4560 ) ;
#11016=EDGE_LOOP ( 'NONE', ( #14059, #3554, #16854, #22026 ) ) ;
#11017=DIRECTION ( 'NONE',  ( -1.982541115402064913E-15, -6.814985084194598285E-15, 1.000000000000000000 ) ) ;
#11024=CARTESIAN_POINT ( 'NONE',  ( 120.8143550994449953, 2.935590694028680225, 13.00000000000000000 ) ) ;
#11026=EDGE_LOOP ( 'NONE', ( #18333, #16500 ) ) ;
#11029=ORIENTED_EDGE ( 'NONE', *, *, #11985, .T. ) ;
#11036=DIRECTION ( 'NONE',  ( -2.670035496199930325E-15, -1.152311220646620054E-14, 1.000000000000000000 ) ) ;
#11037=VERTEX_POINT ( 'NONE', #13454 ) ;
#11043=VERTEX_POINT ( 'NONE', #22109 ) ;
#11046=ORIENTED_EDGE ( 'NONE', *, *, #11985, .F. ) ;
#11049=VECTOR ( 'NONE', #16829, 1000.000000000000227 ) ;
#11050=FACE_OUTER_BOUND ( 'NONE', #15402, .T. ) ;
#11055=CARTESIAN_POINT ( 'NONE',  ( 118.5079952955230027, -6.794810348829399160, 15.50000000000000000 ) ) ;
#11061=LINE ( 'NONE', #4030, #20377 ) ;
#11065=DIRECTION ( 'NONE',  ( -0.2306359803922066187, -0.9730401042858026761, 0.000000000000000000 ) ) ;
#11066=DIRECTION ( 'NONE',  ( -0.2306359803922080620, -0.9730401042858023430, -1.182825655742500503E-14 ) ) ;
#11076=DIRECTION ( 'NONE',  ( 0.9730401042858024541, -0.2306359803922080898, -5.959266323858942451E-17 ) ) ;
#11082=EDGE_CURVE ( 'NONE', #2588, #12472, #11690, .T. ) ;
#11085=ORIENTED_EDGE ( 'NONE', *, *, #6331, .T. ) ;
#11092=CARTESIAN_POINT ( 'NONE',  ( 113.2033677465029911, -29.17473274740290279, -3.099999999999920153 ) ) ;
#11099=DIRECTION ( 'NONE',  ( -7.664170260637049561E-16, -3.491853980616970288E-15, 1.000000000000000000 ) ) ;
#11114=CONICAL_SURFACE ( 'NONE', #462, 2.283500000000000529, 0.7853981633974469467 ) ;
#11122=EDGE_CURVE ( 'NONE', #16084, #7551, #13541, .T. ) ;
#11124=LINE ( 'NONE', #18356, #5221 ) ;
#11130=CARTESIAN_POINT ( 'NONE',  ( 113.4570673249340018, -28.10438863268850085, 2.700000000000049916 ) ) ;
#11139=ORIENTED_EDGE ( 'NONE', *, *, #22385, .F. ) ;
#11146=VERTEX_POINT ( 'NONE', #4417 ) ;
#11147=CARTESIAN_POINT ( 'NONE',  ( 37.88245768368250310, -4.127756955731490152, -13.00000000000000000 ) ) ;
#11148=AXIS2_PLACEMENT_3D ( 'NONE', #5628, #16095, #20117 ) ;
#11151=VECTOR ( 'NONE', #6647, 1000.000000000000227 ) ;
#11159=CIRCLE ( 'NONE', #880, 0.4000000000000001887 ) ;
#11160=ADVANCED_FACE ( 'NONE', ( #9538 ), #16760, .F. ) ;
#11161=EDGE_LOOP ( 'NONE', ( #10226, #10571, #17346, #14204 ) ) ;
#11169=CARTESIAN_POINT ( 'NONE',  ( 113.8430260960419957, 8.210644904773758412, 3.037748485030009753E-14 ) ) ;
#11170=LINE ( 'NONE', #14809, #21312 ) ;
#11197=ORIENTED_EDGE ( 'NONE', *, *, #19547, .T. ) ;
#11217=CIRCLE ( 'NONE', #10075, 2.999999999999999556 ) ;
#11220=CARTESIAN_POINT ( 'NONE',  ( 51.98156320189710300, 17.12649442102254937, -13.00000000000000000 ) ) ;
#11226=CARTESIAN_POINT ( 'NONE',  ( 120.6036919168680015, 2.985523383783529994, -13.00000000000000000 ) ) ;
#11237=CYLINDRICAL_SURFACE ( 'NONE', #18879, 2.066999999999999726 ) ;
#11242=CYLINDRICAL_SURFACE ( 'NONE', #13066, 0.4000000000000001887 ) ;
#11243=FACE_OUTER_BOUND ( 'NONE', #22420, .T. ) ;
#11270=LINE ( 'NONE', #13614, #18162 ) ;
#11287=EDGE_CURVE ( 'NONE', #18309, #4396, #6755, .T. ) ;
#11292=EDGE_CURVE ( 'NONE', #14346, #5109, #12271, .T. ) ;
#11299=AXIS2_PLACEMENT_3D ( 'NONE', #7536, #382, #2177 ) ;
#11301=FACE_OUTER_BOUND ( 'NONE', #20396, .T. ) ;
#11317=EDGE_CURVE ( 'NONE', #13027, #21933, #2943, .T. ) ;
#11328=AXIS2_PLACEMENT_3D ( 'NONE', #23345, #14445, #21800 ) ;
#11335=CIRCLE ( 'NONE', #1820, 12.49999999999999467 ) ;
#11339=CARTESIAN_POINT ( 'NONE',  ( 61.45890873801150178, 17.00438549795339682, 13.00000000000000000 ) ) ;
#11342=CARTESIAN_POINT ( 'NONE',  ( 117.1241794131700118, -12.63305097454420078, 15.50000000000000000 ) ) ;
#11352=DIRECTION ( 'NONE',  ( 0.2306359803922085339, 0.9730401042858022320, 0.000000000000000000 ) ) ;
#11356=DIRECTION ( 'NONE',  ( -0.9730401042858022320, 0.2306359803922080343, 5.959266323858941219E-17 ) ) ;
#11359=CARTESIAN_POINT ( 'NONE',  ( 41.24356139695900225, 11.92996613406550033, -18.89999999999999858 ) ) ;
#11362=LINE ( 'NONE', #11609, #8781 ) ;
#11368=ORIENTED_EDGE ( 'NONE', *, *, #19285, .F. ) ;
#11372=CARTESIAN_POINT ( 'NONE',  ( 120.8143550994449953, 2.935590694028680225, 13.00000000000000000 ) ) ;
#11391=VERTEX_POINT ( 'NONE', #14372 ) ;
#11393=ORIENTED_EDGE ( 'NONE', *, *, #19706, .T. ) ;
#11398=ORIENTED_EDGE ( 'NONE', *, *, #7871, .F. ) ;
#11400=CIRCLE ( 'NONE', #12165, 0.4000000000000001887 ) ;
#11406=CIRCLE ( 'NONE', #1132, 6.999999999999997335 ) ;
#11411=EDGE_CURVE ( 'NONE', #4396, #19560, #12379, .T. ) ;
#11412=EDGE_CURVE ( 'NONE', #18262, #8564, #23277, .T. ) ;
#11442=CIRCLE ( 'NONE', #10733, 2.499999999999999112 ) ;
#11446=EDGE_CURVE ( 'NONE', #23127, #11146, #16975, .T. ) ;
#11449=LINE ( 'NONE', #5953, #15864 ) ;
#11470=ADVANCED_FACE ( 'NONE', ( #3785 ), #19624, .F. ) ;
#11471=LINE ( 'NONE', #16538, #22639 ) ;
#11473=DIRECTION ( 'NONE',  ( 1.000000000000000000, -8.255079201972930249E-15, 0.000000000000000000 ) ) ;
#11478=ADVANCED_FACE ( 'NONE', ( #18060 ), #5123, .F. ) ;
#11486=DIRECTION ( 'NONE',  ( 0.2306359803921919083, 0.9730401042858062288, 1.301042606982611127E-13 ) ) ;
#11490=ORIENTED_EDGE ( 'NONE', *, *, #10188, .T. ) ;
#11494=CONICAL_SURFACE ( 'NONE', #5391, 1.033499999999999863, 1.029744258676650093 ) ;
#11495=AXIS2_PLACEMENT_3D ( 'NONE', #5911, #16702, #7232 ) ;
#11497=ORIENTED_EDGE ( 'NONE', *, *, #3594, .T. ) ;
#11505=AXIS2_PLACEMENT_3D ( 'NONE', #14644, #9065, #19988 ) ;
#11514=EDGE_LOOP ( 'NONE', ( #1187, #11398, #11557, #1929 ) ) ;
#11518=CYLINDRICAL_SURFACE ( 'NONE', #3807, 2.066999999999997950 ) ;
#11523=ADVANCED_FACE ( 'NONE', ( #21388 ), #8809, .T. ) ;
#11528=VECTOR ( 'NONE', #13287, 1000.000000000000227 ) ;
#11533=ORIENTED_EDGE ( 'NONE', *, *, #17800, .T. ) ;
#11542=AXIS2_PLACEMENT_3D ( 'NONE', #3376, #1590, #7424 ) ;
#11556=ORIENTED_EDGE ( 'NONE', *, *, #16305, .F. ) ;
#11557=ORIENTED_EDGE ( 'NONE', *, *, #323, .T. ) ;
#11563=CARTESIAN_POINT ( 'NONE',  ( 120.2377651484647032, 0.5029904333151411500, -13.00000000000000000 ) ) ;
#11581=ORIENTED_EDGE ( 'NONE', *, *, #18059, .F. ) ;
#11591=ORIENTED_EDGE ( 'NONE', *, *, #10118, .F. ) ;
#11595=EDGE_CURVE ( 'NONE', #13995, #14120, #9385, .T. ) ;
#11599=EDGE_CURVE ( 'NONE', #1063, #3048, #4079, .T. ) ;
#11609=CARTESIAN_POINT ( 'NONE',  ( 39.83668191656649782, 5.994421497922050257, 19.59999999999999787 ) ) ;
#11613=ORIENTED_EDGE ( 'NONE', *, *, #13415, .T. ) ;
#11634=CARTESIAN_POINT ( 'NONE',  ( 39.83668191656649782, 5.994421497922050257, 19.59999999999999787 ) ) ;
#11660=CARTESIAN_POINT ( 'NONE',  ( 117.8160873543469904, -9.713930661686799084, 3.415130773183659557E-14 ) ) ;
#11674=CONICAL_SURFACE ( 'NONE', #10912, 2.283499999999998753, 0.7853981633974433940 ) ;
#11681=VERTEX_POINT ( 'NONE', #456 ) ;
#11690=LINE ( 'NONE', #18450, #1410 ) ;
#11694=DIRECTION ( 'NONE',  ( 6.124378941434239724E-17, -2.274246353359159970E-33, 1.000000000000000000 ) ) ;
#11696=EDGE_LOOP ( 'NONE', ( #936, #20529, #10811, #18133 ) ) ;
#11697=ORIENTED_EDGE ( 'NONE', *, *, #22186, .T. ) ;
#11698=DIRECTION ( 'NONE',  ( -0.9730401042858024541, 0.2306359803922080898, 5.959266323858942451E-17 ) ) ;
#11700=ORIENTED_EDGE ( 'NONE', *, *, #11317, .T. ) ;
#11703=DIRECTION ( 'NONE',  ( -0.2306359803922080620, -0.9730401042858023430, 6.358253941197272741E-15 ) ) ;
#11728=EDGE_LOOP ( 'NONE', ( #6085, #17545, #6892, #7859 ) ) ;
#11729=FACE_OUTER_BOUND ( 'NONE', #16885, .T. ) ;
#11737=AXIS2_PLACEMENT_3D ( 'NONE', #11924, #8450, #19252 ) ;
#11739=VERTEX_POINT ( 'NONE', #18422 ) ;
#11753=ORIENTED_EDGE ( 'NONE', *, *, #20530, .F. ) ;
#11764=ADVANCED_FACE ( 'NONE', ( #1041 ), #2728, .T. ) ;
#11767=VERTEX_POINT ( 'NONE', #20887 ) ;
#11769=DIRECTION ( 'NONE',  ( -0.2306359803922054252, -0.9730401042858028982, 0.000000000000000000 ) ) ;
#11770=ORIENTED_EDGE ( 'NONE', *, *, #400, .F. ) ;
#11771=CARTESIAN_POINT ( 'NONE',  ( 119.9163041628193440, 1.024182177979823027, -13.00000000000000000 ) ) ;
#11782=EDGE_LOOP ( 'NONE', ( #1342, #6354, #22927, #14968 ) ) ;
#11791=AXIS2_PLACEMENT_3D ( 'NONE', #9097, #18132, #17695 ) ;
#11798=ORIENTED_EDGE ( 'NONE', *, *, #12888, .F. ) ;
#11800=DIRECTION ( 'NONE',  ( -0.9730401042858024541, 0.2306359803922080898, 5.959266323858942451E-17 ) ) ;
#11808=ORIENTED_EDGE ( 'NONE', *, *, #16491, .T. ) ;
#11815=DIRECTION ( 'NONE',  ( -1.115264941341835834E-15, 3.837966487416229483E-32, -1.000000000000000000 ) ) ;
#11825=DIRECTION ( 'NONE',  ( -0.9730401042858024541, 0.2306359803922080898, 5.959266323858942451E-17 ) ) ;
#11826=CARTESIAN_POINT ( 'NONE',  ( 35.93893384793820189, -10.44995626450799975, 3.100000000000000089 ) ) ;
#11827=DIRECTION ( 'NONE',  ( -0.9730401042858024541, 0.2306359803922080898, 5.959266323858942451E-17 ) ) ;
#11829=CARTESIAN_POINT ( 'NONE',  ( 118.4388045014059969, -7.086722380115159758, -19.59999999999999787 ) ) ;
#11844=DIRECTION ( 'NONE',  ( 0.2306359803922094498, 0.9730401042858018990, 0.000000000000000000 ) ) ;
#11853=CARTESIAN_POINT ( 'NONE',  ( 53.20239347634441884, 27.69690417850089759, 2.500000000000052847 ) ) ;
#11864=VECTOR ( 'NONE', #8888, 1000.000000000000227 ) ;
#11872=CONICAL_SURFACE ( 'NONE', #12982, 2.283500000000000085, 0.7853981633974469467 ) ;
#11873=CARTESIAN_POINT ( 'NONE',  ( 37.46113131852679601, -4.027891576221660053, -13.00000000000000000 ) ) ;
#11874=VERTEX_POINT ( 'NONE', #11771 ) ;
#11885=VECTOR ( 'NONE', #21605, 1000.000000000000227 ) ;
#11886=CIRCLE ( 'NONE', #16787, 12.50000000000000000 ) ;
#11895=CYLINDRICAL_SURFACE ( 'NONE', #7648, 7.000000000000000888 ) ;
#11896=LINE ( 'NONE', #12005, #16171 ) ;
#11907=AXIS2_PLACEMENT_3D ( 'NONE', #7634, #7759, #18698 ) ;
#11912=ORIENTED_EDGE ( 'NONE', *, *, #11411, .T. ) ;
#11918=DIRECTION ( 'NONE',  ( -0.9730401042858024541, 0.2306359803922080898, 5.959266323858942451E-17 ) ) ;
#11924=CARTESIAN_POINT ( 'NONE',  ( 115.8700071457750056, -9.252658700902388844, 3.427049305831379237E-14 ) ) ;
#11941=DIRECTION ( 'NONE',  ( -3.469446951953605354E-14, -1.084202172485501657E-13, 1.000000000000000000 ) ) ;
#11946=DIRECTION ( 'NONE',  ( -0.9730401042858024541, 0.2306359803922080898, 5.959266323858942451E-17 ) ) ;
#11947=DIRECTION ( 'NONE',  ( -0.2306359803922085339, -0.9730401042858022320, 0.000000000000000000 ) ) ;
#11951=FACE_OUTER_BOUND ( 'NONE', #10334, .T. ) ;
#11955=PLANE ( 'NONE',  #5568 ) ;
#11967=ORIENTED_EDGE ( 'NONE', *, *, #14009, .T. ) ;
#11968=CARTESIAN_POINT ( 'NONE',  ( 55.46237324781409939, -8.294657213477510282, 13.00000000000000000 ) ) ;
#11973=CARTESIAN_POINT ( 'NONE',  ( 36.88454136754629076, -6.460491836936111731, -13.00000000000000000 ) ) ;
#11985=EDGE_CURVE ( 'NONE', #5109, #16036, #13964, .T. ) ;
#12005=CARTESIAN_POINT ( 'NONE',  ( 112.2904587062726876, 7.080247408215292637, -13.00000000000000000 ) ) ;
#12008=EDGE_CURVE ( 'NONE', #21187, #15073, #6773, .T. ) ;
#12015=ORIENTED_EDGE ( 'NONE', *, *, #17909, .T. ) ;
#12040=CARTESIAN_POINT ( 'NONE',  ( 118.5310588935630136, -6.697506338400830650, -19.59999999999999787 ) ) ;
#12044=EDGE_LOOP ( 'NONE', ( #20995, #7631, #5542, #6439 ) ) ;
#12051=CARTESIAN_POINT ( 'NONE',  ( 39.67523673029199927, 5.313293424922040487, -15.90000000000000036 ) ) ;
#12081=CARTESIAN_POINT ( 'NONE',  ( 114.6071564266699880, -22.31351932764730250, 13.00000000000000000 ) ) ;
#12088=FACE_OUTER_BOUND ( 'NONE', #11514, .T. ) ;
#12094=DIRECTION ( 'NONE',  ( -1.000000000000000000, 0.000000000000000000, -1.304396158928240120E-15 ) ) ;
#12111=VECTOR ( 'NONE', #21810, 1000.000000000000227 ) ;
#12114=EDGE_LOOP ( 'NONE', ( #14232, #17664, #2226, #11393 ) ) ;
#12115=EDGE_LOOP ( 'NONE', ( #11085, #8467, #22435, #9004 ) ) ;
#12128=ORIENTED_EDGE ( 'NONE', *, *, #13624, .F. ) ;
#12137=DIRECTION ( 'NONE',  ( -0.9730401042858023430, 0.2306359803922080620, 5.959266323858944916E-17 ) ) ;
#12140=ORIENTED_EDGE ( 'NONE', *, *, #7073, .F. ) ;
#12143=CIRCLE ( 'NONE', #9466, 2.499999999999998224 ) ;
#12151=DIRECTION ( 'NONE',  ( -0.9730401042858024541, 0.2306359803922080898, 5.959266323858942451E-17 ) ) ;
#12165=AXIS2_PLACEMENT_3D ( 'NONE', #10064, #4463, #1116 ) ;
#12175=VECTOR ( 'NONE', #23401, 1000.000000000000000 ) ;
#12178=CARTESIAN_POINT ( 'NONE',  ( 37.46113131852679601, -4.027891576221660053, -13.00000000000000000 ) ) ;
#12187=PLANE ( 'NONE',  #10997 ) ;
#12188=ORIENTED_EDGE ( 'NONE', *, *, #1280, .T. ) ;
#12190=DIRECTION ( 'NONE',  ( -0.2306359803921919083, -0.9730401042858062288, 2.222614453595293935E-13 ) ) ;
#12209=PLANE ( 'NONE',  #15083 ) ;
#12235=EDGE_CURVE ( 'NONE', #19161, #3952, #2812, .T. ) ;
#12236=EDGE_LOOP ( 'NONE', ( #9213, #10458, #12240, #12337 ) ) ;
#12240=ORIENTED_EDGE ( 'NONE', *, *, #7656, .T. ) ;
#12246=DIRECTION ( 'NONE',  ( -0.9730401042858024541, 0.2306359803922080898, 5.959266323858942451E-17 ) ) ;
#12247=ORIENTED_EDGE ( 'NONE', *, *, #16491, .F. ) ;
#12256=CIRCLE ( 'NONE', #6539, 2.500000000000000000 ) ;
#12257=CARTESIAN_POINT ( 'NONE',  ( 113.2320189960273495, -11.71050705297551531, 3.443204550052153714E-14 ) ) ;
#12261=EDGE_CURVE ( 'NONE', #12703, #21124, #13731, .T. ) ;
#12269=AXIS2_PLACEMENT_3D ( 'NONE', #2284, #11698, #15110 ) ;
#12271=LINE ( 'NONE', #23149, #20383 ) ;
#12272=AXIS2_PLACEMENT_3D ( 'NONE', #11372, #9100, #11017 ) ;
#12274=LINE ( 'NONE', #21041, #17564 ) ;
#12276=DIRECTION ( 'NONE',  ( -0.2306359803922094498, -0.9730401042858020100, 1.412237191019847142E-17 ) ) ;
#12278=ADVANCED_FACE ( 'NONE', ( #1593 ), #17876, .T. ) ;
#12295=ADVANCED_FACE ( 'NONE', ( #8971 ), #10648, .F. ) ;
#12298=VECTOR ( 'NONE', #2139, 1000.000000000000227 ) ;
#12299=DIRECTION ( 'NONE',  ( 1.734723475976802677E-14, 4.336808689942006376E-14, 1.000000000000000000 ) ) ;
#12303=CARTESIAN_POINT ( 'NONE',  ( 39.76749112244880280, 5.702509466636339397, 15.50000000000000000 ) ) ;
#12308=LINE ( 'NONE', #1224, #20210 ) ;
#12312=VERTEX_POINT ( 'NONE', #7192 ) ;
#12317=DIRECTION ( 'NONE',  ( 2.670035496199930325E-15, 1.152311220646620054E-14, -1.000000000000000000 ) ) ;
#12323=CIRCLE ( 'NONE', #5097, 2.066999999999999726 ) ;
#12324=DIRECTION ( 'NONE',  ( 7.515353331921825981E-30, -5.761557392270000270E-15, 1.000000000000000000 ) ) ;
#12330=VERTEX_POINT ( 'NONE', #12426 ) ;
#12333=VERTEX_POINT ( 'NONE', #3505 ) ;
#12337=ORIENTED_EDGE ( 'NONE', *, *, #11001, .F. ) ;
#12347=LINE ( 'NONE', #19678, #15464 ) ;
#12350=DIRECTION ( 'NONE',  ( -0.9730401042858024541, 0.2306359803922080898, 5.959266323859062013E-17 ) ) ;
#12358=ORIENTED_EDGE ( 'NONE', *, *, #21765, .T. ) ;
#12359=EDGE_CURVE ( 'NONE', #22197, #12472, #9797, .T. ) ;
#12360=CARTESIAN_POINT ( 'NONE',  ( 114.2412296582674429, -24.79605227811687485, 13.00000000000000000 ) ) ;
#12361=DIRECTION ( 'NONE',  ( 0.9730401042858024541, -0.2306359803922080898, -5.959266323858592394E-17 ) ) ;
#12362=ORIENTED_EDGE ( 'NONE', *, *, #5172, .F. ) ;
#12377=VERTEX_POINT ( 'NONE', #14305 ) ;
#12379=LINE ( 'NONE', #16041, #3698 ) ;
#12390=DIRECTION ( 'NONE',  ( 0.2306359803922080898, 0.9730401042858024541, -2.572202231434325988E-16 ) ) ;
#12394=AXIS2_PLACEMENT_3D ( 'NONE', #4166, #15089, #22322 ) ;
#12395=LINE ( 'NONE', #15716, #12175 ) ;
#12400=DIRECTION ( 'NONE',  ( -0.9730401042858022320, 0.2306359803922080343, 5.959266323858941219E-17 ) ) ;
#12402=CARTESIAN_POINT ( 'NONE',  ( 41.08211621068439712, 11.24883806106539907, 18.89999999999999858 ) ) ;
#12403=AXIS2_PLACEMENT_3D ( 'NONE', #13940, #23065, #4686 ) ;
#12406=EDGE_LOOP ( 'NONE', ( #3719, #18042 ) ) ;
#12412=CARTESIAN_POINT ( 'NONE',  ( 36.88454136754629786, -6.460491836936129495, -2.999999999999930278 ) ) ;
#12414=VERTEX_POINT ( 'NONE', #9690 ) ;
#12415=CARTESIAN_POINT ( 'NONE',  ( 122.4288069621910040, 9.746871424029301068, 13.00000000000000000 ) ) ;
#12418=DIRECTION ( 'NONE',  ( -0.9730401042858024541, 0.2306359803922080898, 5.959266323862942222E-17 ) ) ;
#12422=VECTOR ( 'NONE', #1768, 1000.000000000000114 ) ;
#12426=CARTESIAN_POINT ( 'NONE',  ( 120.8143550994449953, 2.935590694028619829, -20.00000000000000000 ) ) ;
#12430=FACE_OUTER_BOUND ( 'NONE', #5900, .T. ) ;
#12462=DIRECTION ( 'NONE',  ( 0.2306359803922053142, 0.9730401042858028982, 0.000000000000000000 ) ) ;
#12472=VERTEX_POINT ( 'NONE', #16656 ) ;
#12475=CIRCLE ( 'NONE', #7535, 0.3999999999999998557 ) ;
#12479=EDGE_CURVE ( 'NONE', #6410, #22407, #16905, .T. ) ;
#12481=( NAMED_UNIT ( * ) SI_UNIT ( $, .STERADIAN. ) SOLID_ANGLE_UNIT ( ) );
#12494=ORIENTED_EDGE ( 'NONE', *, *, #3740, .T. ) ;
#12506=LINE ( 'NONE', #19740, #22003 ) ;
#12518=DIRECTION ( 'NONE',  ( -0.9730401042858024541, 0.2306359803922080898, 5.959266323859172946E-17 ) ) ;
#12526=LINE ( 'NONE', #7416, #22725 ) ;
#12527=AXIS2_PLACEMENT_3D ( 'NONE', #6470, #15738, #6721 ) ;
#12534=DIRECTION ( 'NONE',  ( -0.9730401042858024541, 0.2306359803922080898, 5.959266323858952312E-17 ) ) ;
#12539=LINE ( 'NONE', #16098, #17243 ) ;
#12542=DIRECTION ( 'NONE',  ( -0.9730401042858024541, 0.2306359803922080898, 5.959266323858942451E-17 ) ) ;
#12555=EDGE_CURVE ( 'NONE', #15043, #15812, #11124, .T. ) ;
#12569=ORIENTED_EDGE ( 'NONE', *, *, #5584, .T. ) ;
#12576=CARTESIAN_POINT ( 'NONE',  ( 114.3964932440919995, -22.26358663789240211, -13.00000000000000000 ) ) ;
#12583=ORIENTED_EDGE ( 'NONE', *, *, #644, .T. ) ;
#12587=ADVANCED_FACE ( 'NONE', ( #11951 ), #1030, .F. ) ;
#12595=DIRECTION ( 'NONE',  ( 0.9730401042858021210, -0.2306359803922085061, 0.000000000000000000 ) ) ;
#12597=PLANE ( 'NONE',  #15752 ) ;
#12646=CYLINDRICAL_SURFACE ( 'NONE', #11505, 2.066999999999999726 ) ;
#12647=EDGE_CURVE ( 'NONE', #9648, #3048, #20934, .T. ) ;
#12656=ORIENTED_EDGE ( 'NONE', *, *, #20098, .T. ) ;
#12658=DIRECTION ( 'NONE',  ( 0.2306359803922076457, 0.9730401042858025651, 0.000000000000000000 ) ) ;
#12669=DIRECTION ( 'NONE',  ( 0.2306359803922080898, 0.9730401042858024541, -2.572202231434325988E-16 ) ) ;
#12677=ORIENTED_EDGE ( 'NONE', *, *, #8399, .T. ) ;
#12685=EDGE_CURVE ( 'NONE', #15635, #813, #12475, .T. ) ;
#12703=VERTEX_POINT ( 'NONE', #21169 ) ;
#12710=CYLINDRICAL_SURFACE ( 'NONE', #7784, 0.4000000000000010214 ) ;
#12736=DIRECTION ( 'NONE',  ( 9.055045682909269434E-14, 0.000000000000000000, -1.000000000000000000 ) ) ;
#12739=AXIS2_PLACEMENT_3D ( 'NONE', #2569, #13380, #415 ) ;
#12741=EDGE_CURVE ( 'NONE', #3857, #503, #11335, .T. ) ;
#12751=ORIENTED_EDGE ( 'NONE', *, *, #675, .F. ) ;
#12759=EDGE_CURVE ( 'NONE', #4396, #18309, #6782, .T. ) ;
#12770=EDGE_CURVE ( 'NONE', #19953, #7688, #3471, .T. ) ;
#12779=ORIENTED_EDGE ( 'NONE', *, *, #20948, .F. ) ;
#12790=AXIS2_PLACEMENT_3D ( 'NONE', #17275, #13703, #12299 ) ;
#12806=ADVANCED_FACE ( 'NONE', ( #18082 ), #10746, .T. ) ;
#12812=ORIENTED_EDGE ( 'NONE', *, *, #22952, .T. ) ;
#12814=AXIS2_PLACEMENT_3D ( 'NONE', #1068, #15570, #21039 ) ;
#12817=FACE_OUTER_BOUND ( 'NONE', #11161, .T. ) ;
#12820=FACE_OUTER_BOUND ( 'NONE', #7269, .T. ) ;
#12843=EDGE_CURVE ( 'NONE', #13304, #23125, #8836, .T. ) ;
#12844=DIRECTION ( 'NONE',  ( -0.2306359803922080898, -0.9730401042858024541, 2.572202231434325988E-16 ) ) ;
#12847=ORIENTED_EDGE ( 'NONE', *, *, #5076, .F. ) ;
#12855=DIRECTION ( 'NONE',  ( 0.2306359803922083396, 0.9730401042858023430, 1.301042606982605826E-13 ) ) ;
#12858=DIRECTION ( 'NONE',  ( -0.2306359803922087282, -0.9730401042858021210, 5.204170427930421283E-15 ) ) ;
#12865=ORIENTED_EDGE ( 'NONE', *, *, #1703, .T. ) ;
#12866=EDGE_CURVE ( 'NONE', #1999, #16389, #16175, .T. ) ;
#12867=FACE_OUTER_BOUND ( 'NONE', #19977, .T. ) ;
#12888=EDGE_CURVE ( 'NONE', #14815, #8021, #11449, .T. ) ;
#12890=CARTESIAN_POINT ( 'NONE',  ( 113.4570673249340018, -28.10438863268850085, -2.700000000000000178 ) ) ;
#12891=CARTESIAN_POINT ( 'NONE',  ( 37.46113131852679601, -4.027891576221680481, -13.00000000000000000 ) ) ;
#12907=ORIENTED_EDGE ( 'NONE', *, *, #6029, .F. ) ;
#12910=ORIENTED_EDGE ( 'NONE', *, *, #6328, .F. ) ;
#12920=ORIENTED_EDGE ( 'NONE', *, *, #5597, .T. ) ;
#12926=AXIS2_PLACEMENT_3D ( 'NONE', #22623, #771, #7922 ) ;
#12941=ORIENTED_EDGE ( 'NONE', *, *, #6334, .F. ) ;
#12948=VERTEX_POINT ( 'NONE', #358 ) ;
#12951=ORIENTED_EDGE ( 'NONE', *, *, #5222, .F. ) ;
#12960=CARTESIAN_POINT ( 'NONE',  ( 117.1241794131700118, -12.63305097454420078, 15.50000000000000000 ) ) ;
#12971=EDGE_CURVE ( 'NONE', #15644, #21038, #15096, .T. ) ;
#12975=CIRCLE ( 'NONE', #19439, 2.499999999999998224 ) ;
#12976=VECTOR ( 'NONE', #1260, 1000.000000000000227 ) ;
#12982=AXIS2_PLACEMENT_3D ( 'NONE', #11226, #14872, #16766 ) ;
#12986=VECTOR ( 'NONE', #2254, 1000.000000000000227 ) ;
#12990=ORIENTED_EDGE ( 'NONE', *, *, #21135, .T. ) ;
#13017=LINE ( 'NONE', #14431, #2360 ) ;
#13021=VECTOR ( 'NONE', #15933, 1000.000000000000227 ) ;
#13025=EDGE_LOOP ( 'NONE', ( #591, #5413 ) ) ;
#13026=CARTESIAN_POINT ( 'NONE',  ( 35.93893384793820189, -10.44995626450799975, 2.700000000000000178 ) ) ;
#13027=VERTEX_POINT ( 'NONE', #16874 ) ;
#13063=CARTESIAN_POINT ( 'NONE',  ( 36.88454136754619128, -6.460491836936199661, 3.000000000000000000 ) ) ;
#13065=DIRECTION ( 'NONE',  ( 0.2306359803922076457, 0.9730401042858023430, 0.000000000000000000 ) ) ;
#13066=AXIS2_PLACEMENT_3D ( 'NONE', #6103, #4089, #869 ) ;
#13082=VERTEX_POINT ( 'NONE', #7981 ) ;
#13104=CARTESIAN_POINT ( 'NONE',  ( 117.1933702072879981, -12.34113894325849969, -18.89999999999999858 ) ) ;
#13110=CYLINDRICAL_SURFACE ( 'NONE', #12269, 4.999999999999996447 ) ;
#13125=CARTESIAN_POINT ( 'NONE',  ( 114.8732178155626826, -20.25231274233364687, -13.00000000000000000 ) ) ;
#13133=VERTEX_POINT ( 'NONE', #6419 ) ;
#13135=FACE_OUTER_BOUND ( 'NONE', #21156, .T. ) ;
#13158=ADVANCED_FACE ( 'NONE', ( #20906 ), #15213, .F. ) ;
#13173=EDGE_CURVE ( 'NONE', #21550, #15073, #2973, .T. ) ;
#13183=DIRECTION ( 'NONE',  ( 0.000000000000000000, 0.000000000000000000, -1.000000000000000000 ) ) ;
#13187=CARTESIAN_POINT ( 'NONE',  ( 114.2412296582679971, -24.79605227811680379, 3.000000000000000000 ) ) ;
#13200=CARTESIAN_POINT ( 'NONE',  ( 122.4288069621910040, 9.746871424029301068, 13.00000000000000000 ) ) ;
#13205=FACE_OUTER_BOUND ( 'NONE', #18044, .T. ) ;
#13206=EDGE_CURVE ( 'NONE', #9676, #21726, #7164, .T. ) ;
#13213=VECTOR ( 'NONE', #5490, 1000.000000000000227 ) ;
#13224=EDGE_LOOP ( 'NONE', ( #14125, #19532, #18786, #15216 ) ) ;
#13235=LINE ( 'NONE', #5336, #20227 ) ;
#13267=CARTESIAN_POINT ( 'NONE',  ( 35.93893384793820189, -10.44995626450799975, -2.700000000000000178 ) ) ;
#13277=ADVANCED_FACE ( 'NONE', ( #9114 ), #14343, .T. ) ;
#13284=CARTESIAN_POINT ( 'NONE',  ( 120.8143550994449953, 2.935590694028659797, 13.00000000000000000 ) ) ;
#13287=DIRECTION ( 'NONE',  ( -0.9730401042858022320, 0.2306359803922080343, 5.959266323858941219E-17 ) ) ;
#13288=VERTEX_POINT ( 'NONE', #301 ) ;
#13297=ORIENTED_EDGE ( 'NONE', *, *, #16219, .F. ) ;
#13302=DIRECTION ( 'NONE',  ( -0.9730401042858024541, 0.2306359803922080898, 5.959266323858942451E-17 ) ) ;
#13303=CARTESIAN_POINT ( 'NONE',  ( 53.15246078658950069, 27.48624099592299785, 3.293763653412249631E-14 ) ) ;
#13304=VERTEX_POINT ( 'NONE', #185 ) ;
#13306=CARTESIAN_POINT ( 'NONE',  ( 77.95761363658371579, -13.11276471035541213, 3.659235858378048644E-14 ) ) ;
#13310=ORIENTED_EDGE ( 'NONE', *, *, #8995, .F. ) ;
#13321=VECTOR ( 'NONE', #18723, 1000.000000000000227 ) ;
#13329=EDGE_CURVE ( 'NONE', #11391, #14490, #7346, .T. ) ;
#13333=CARTESIAN_POINT ( 'NONE',  ( 113.4570673249340018, -28.10438863268850085, -3.399999999999949729 ) ) ;
#13335=ORIENTED_EDGE ( 'NONE', *, *, #3818, .T. ) ;
#13337=VECTOR ( 'NONE', #15779, 1000.000000000000227 ) ;
#13342=DIRECTION ( 'NONE',  ( 0.2306359803922076457, 0.9730401042858023430, 0.000000000000000000 ) ) ;
#13346=DIRECTION ( 'NONE',  ( 0.000000000000000000, -4.336808689942006376E-14, -1.000000000000000000 ) ) ;
#13362=CARTESIAN_POINT ( 'NONE',  ( 117.1241794131700118, -12.63305097454420078, -15.90000000000000036 ) ) ;
#13365=EDGE_LOOP ( 'NONE', ( #21586, #8282 ) ) ;
#13366=LINE ( 'NONE', #20482, #10371 ) ;
#13375=LINE ( 'NONE', #16815, #7979 ) ;
#13380=DIRECTION ( 'NONE',  ( 0.000000000000000000, 0.000000000000000000, 1.000000000000000000 ) ) ;
#13387=EDGE_LOOP ( 'NONE', ( #16106, #13453, #4419, #12128 ) ) ;
#13390=AXIS2_PLACEMENT_3D ( 'NONE', #14064, #8378, #19299 ) ;
#13392=ORIENTED_EDGE ( 'NONE', *, *, #3160, .T. ) ;
#13398=CARTESIAN_POINT ( 'NONE',  ( 43.45766680872420551, 21.27115113520920175, -13.00000000000000000 ) ) ;
#13399=AXIS2_PLACEMENT_3D ( 'NONE', #5060, #12324, #3029 ) ;
#13413=CYLINDRICAL_SURFACE ( 'NONE', #568, 12.49999999999999645 ) ;
#13415=EDGE_CURVE ( 'NONE', #21187, #1005, #11270, .T. ) ;
#13453=ORIENTED_EDGE ( 'NONE', *, *, #12971, .T. ) ;
#13454=CARTESIAN_POINT ( 'NONE',  ( 114.1489752661110089, -25.18526831983100323, 3.399999999999999911 ) ) ;
#13457=FACE_BOUND ( 'NONE', #661, .T. ) ;
#13466=FACE_BOUND ( 'NONE', #14631, .T. ) ;
#13469=FACE_OUTER_BOUND ( 'NONE', #15611, .T. ) ;
#13471=FACE_OUTER_BOUND ( 'NONE', #17686, .T. ) ;
#13503=LINE ( 'NONE', #7808, #11049 ) ;
#13505=DIRECTION ( 'NONE',  ( 0.2306359803922080620, 0.9730401042858023430, 5.907067092757398303E-15 ) ) ;
#13508=DIRECTION ( 'NONE',  ( -0.9730401042858024541, 0.2306359803922080898, 5.959266323858942451E-17 ) ) ;
#13538=ORIENTED_EDGE ( 'NONE', *, *, #9731, .T. ) ;
#13541=CIRCLE ( 'NONE', #14684, 2.066999999999999726 ) ;
#13561=CARTESIAN_POINT ( 'NONE',  ( 111.8137341348020044, 5.068973512656589797, 13.00000000000000000 ) ) ;
#13565=EDGE_LOOP ( 'NONE', ( #19853, #22428, #3824, #18678 ) ) ;
#13566=ORIENTED_EDGE ( 'NONE', *, *, #22139, .F. ) ;
#13572=DIRECTION ( 'NONE',  ( 0.9730401042858024541, -0.2306359803922080898, -5.959266323863172718E-17 ) ) ;
#13582=CARTESIAN_POINT ( 'NONE',  ( 37.46113131852679601, -4.027891576221660053, 13.00000000000000000 ) ) ;
#13597=VECTOR ( 'NONE', #10046, 1000.000000000000000 ) ;
#13604=DIRECTION ( 'NONE',  ( -0.2306359803922066187, -0.9730401042858026761, 0.000000000000000000 ) ) ;
#13609=ADVANCED_FACE ( 'NONE', ( #19428 ), #13855, .T. ) ;
#13612=CARTESIAN_POINT ( 'NONE',  ( 41.15130700480209924, 11.54075009235119964, -15.90000000000000036 ) ) ;
#13613=VERTEX_POINT ( 'NONE', #3273 ) ;
#13614=CARTESIAN_POINT ( 'NONE',  ( 37.14513723987899851, -6.299761344113198547, 13.00000000000000000 ) ) ;
#13619=CARTESIAN_POINT ( 'NONE',  ( 105.3404740731333078, -22.24134309433305390, 13.00000000000000000 ) ) ;
#13624=EDGE_CURVE ( 'NONE', #2339, #7183, #2925, .T. ) ;
#13625=DIRECTION ( 'NONE',  ( -0.2306359803922076457, -0.9730401042858025651, 0.000000000000000000 ) ) ;
#13637=CYLINDRICAL_SURFACE ( 'NONE', #22493, 4.999999999999996447 ) ;
#13643=DIRECTION ( 'NONE',  ( -2.347220324585850163E-14, -9.876950852243829821E-14, -1.000000000000000000 ) ) ;
#13644=ORIENTED_EDGE ( 'NONE', *, *, #833, .F. ) ;
#13661=CARTESIAN_POINT ( 'NONE',  ( 44.35571774535060996, 23.18255965125822371, -13.00000000000000000 ) ) ;
#13670=PLANE ( 'NONE',  #16963 ) ;
#13688=ADVANCED_FACE ( 'NONE', ( #6486 ), #12209, .T. ) ;
#13693=CARTESIAN_POINT ( 'NONE',  ( 120.8143550994449953, 2.935590694028619829, -13.00000000000000000 ) ) ;
#13703=DIRECTION ( 'NONE',  ( 0.9730401042858024541, -0.2306359803922080898, -5.959266323863413074E-17 ) ) ;
#13706=DIRECTION ( 'NONE',  ( 1.304396158928310329E-15, 5.761557392270100456E-15, -1.000000000000000000 ) ) ;
#13710=ORIENTED_EDGE ( 'NONE', *, *, #11082, .F. ) ;
#13712=LINE ( 'NONE', #4696, #14145 ) ;
#13721=AXIS2_PLACEMENT_3D ( 'NONE', #7228, #19464, #3194 ) ;
#13723=CIRCLE ( 'NONE', #15990, 0.3999999999999998557 ) ;
#13729=ADVANCED_FACE ( 'NONE', ( #19091 ), #20852, .F. ) ;
#13731=LINE ( 'NONE', #20972, #18131 ) ;
#13733=ORIENTED_EDGE ( 'NONE', *, *, #8699, .T. ) ;
#13745=CARTESIAN_POINT ( 'NONE',  ( 118.4388045014059969, -7.086722380115130449, 18.89999999999999858 ) ) ;
#13764=CARTESIAN_POINT ( 'NONE',  ( 120.0770346556423931, 0.7635863056469410770, 13.00000000000000000 ) ) ;
#13769=DIRECTION ( 'NONE',  ( 0.000000000000000000, 2.478176394252581338E-15, -1.000000000000000000 ) ) ;
#13770=CARTESIAN_POINT ( 'NONE',  ( 102.8131131701580046, 7.202356331284469171, -13.00000000000000000 ) ) ;
#13779=LINE ( 'NONE', #10225, #6846 ) ;
#13785=ORIENTED_EDGE ( 'NONE', *, *, #15435, .T. ) ;
#13795=EDGE_CURVE ( 'NONE', #8608, #11767, #20387, .T. ) ;
#13814=PLANE ( 'NONE',  #8104 ) ;
#13820=CARTESIAN_POINT ( 'NONE',  ( 113.4570673249340018, -28.10438863268850085, 2.700000000000049916 ) ) ;
#13823=CYLINDRICAL_SURFACE ( 'NONE', #5981, 7.000000000000000000 ) ;
#13825=DIRECTION ( 'NONE',  ( -0.2306359803922083396, -0.9730401042858023430, 0.000000000000000000 ) ) ;
#13831=DIRECTION ( 'NONE',  ( -1.982541115402064913E-15, -6.938893903907227589E-15, 1.000000000000000000 ) ) ;
#13835=ORIENTED_EDGE ( 'NONE', *, *, #14345, .F. ) ;
#13846=DIRECTION ( 'NONE',  ( -0.9730401042858024541, 0.2306359803922080898, 5.959266323858942451E-17 ) ) ;
#13855=PLANE ( 'NONE',  #23408 ) ;
#13857=CIRCLE ( 'NONE', #3235, 2.499999999999999112 ) ;
#13858=ORIENTED_EDGE ( 'NONE', *, *, #6331, .F. ) ;
#13862=CARTESIAN_POINT ( 'NONE',  ( 114.6158348783805963, -5.872266427260702137, 3.471470530880454566E-14 ) ) ;
#13863=ORIENTED_EDGE ( 'NONE', *, *, #5288, .T. ) ;
#13865=ADVANCED_FACE ( 'NONE', ( #7196 ), #8652, .F. ) ;
#13874=CONICAL_SURFACE ( 'NONE', #975, 2.283500000000000085, 0.7853981633974447263 ) ;
#13880=CARTESIAN_POINT ( 'NONE',  ( 43.45766680872420551, 21.27115113520920175, 13.00000000000000000 ) ) ;
#13887=EDGE_LOOP ( 'NONE', ( #9866, #21882 ) ) ;
#13888=VERTEX_POINT ( 'NONE', #21898 ) ;
#13891=EDGE_CURVE ( 'NONE', #15201, #9834, #16573, .T. ) ;
#13923=CARTESIAN_POINT ( 'NONE',  ( 114.3964932440919995, -22.26358663789240211, 13.00000000000000000 ) ) ;
#13938=LINE ( 'NONE', #22836, #9770 ) ;
#13940=CARTESIAN_POINT ( 'NONE',  ( 117.1011158151309957, -12.73035498497280038, 20.00000000000000000 ) ) ;
#13943=ORIENTED_EDGE ( 'NONE', *, *, #11001, .T. ) ;
#13947=DIRECTION ( 'NONE',  ( -0.9730401042858022320, 0.2306359803922080343, 5.959266323858941219E-17 ) ) ;
#13956=FACE_OUTER_BOUND ( 'NONE', #21756, .T. ) ;
#13964=CIRCLE ( 'NONE', #23427, 0.3999999999999982458 ) ;
#13981=CARTESIAN_POINT ( 'NONE',  ( 117.0319250210129951, -13.02226701625849969, -18.89999999999999858 ) ) ;
#13995=VERTEX_POINT ( 'NONE', #4341 ) ;
#14002=EDGE_LOOP ( 'NONE', ( #9467, #18375, #8159, #4915 ) ) ;
#14009=EDGE_CURVE ( 'NONE', #21124, #20573, #9919, .T. ) ;
#14019=ORIENTED_EDGE ( 'NONE', *, *, #18059, .T. ) ;
#14025=ORIENTED_EDGE ( 'NONE', *, *, #4604, .T. ) ;
#14034=ORIENTED_EDGE ( 'NONE', *, *, #619, .F. ) ;
#14047=ADVANCED_FACE ( 'NONE', ( #11243 ), #1050, .F. ) ;
#14059=ORIENTED_EDGE ( 'NONE', *, *, #10155, .T. ) ;
#14064=CARTESIAN_POINT ( 'NONE',  ( 120.8143550994449953, 2.935590694028629599, 20.00000000000000000 ) ) ;
#14083=DIRECTION ( 'NONE',  ( 0.000000000000000000, 2.478176394252581338E-15, -1.000000000000000000 ) ) ;
#14098=DIRECTION ( 'NONE',  ( 0.9730401042858024541, -0.2306359803922080898, -5.959266323858472832E-17 ) ) ;
#14118=DIRECTION ( 'NONE',  ( -1.173102895937339952E-16, -2.365413804416879953E-16, -1.000000000000000000 ) ) ;
#14120=VERTEX_POINT ( 'NONE', #22492 ) ;
#14125=ORIENTED_EDGE ( 'NONE', *, *, #14245, .F. ) ;
#14129=VECTOR ( 'NONE', #21734, 1000.000000000000227 ) ;
#14145=VECTOR ( 'NONE', #20232, 1000.000000000000227 ) ;
#14146=ADVANCED_FACE ( 'NONE', ( #982 ), #11955, .T. ) ;
#14157=VERTEX_POINT ( 'NONE', #4685 ) ;
#14161=CIRCLE ( 'NONE', #6974, 2.066999999999999726 ) ;
#14181=VECTOR ( 'NONE', #23040, 1000.000000000000000 ) ;
#14190=EDGE_CURVE ( 'NONE', #2314, #20573, #15365, .T. ) ;
#14204=ORIENTED_EDGE ( 'NONE', *, *, #892, .T. ) ;
#14205=DIRECTION ( 'NONE',  ( -0.2306359803922054252, -0.9730401042858028982, 0.000000000000000000 ) ) ;
#14220=EDGE_CURVE ( 'NONE', #7551, #23127, #15722, .T. ) ;
#14231=DIRECTION ( 'NONE',  ( 0.2306359803922080620, 0.9730401042858023430, 2.536240390523813244E-14 ) ) ;
#14232=ORIENTED_EDGE ( 'NONE', *, *, #21307, .F. ) ;
#14236=ORIENTED_EDGE ( 'NONE', *, *, #17909, .F. ) ;
#14237=ORIENTED_EDGE ( 'NONE', *, *, #5597, .F. ) ;
#14245=EDGE_CURVE ( 'NONE', #11874, #6605, #13938, .T. ) ;
#14251=CARTESIAN_POINT ( 'NONE',  ( 53.10252809683457542, 27.27557781334508036, -2.066999999999924231 ) ) ;
#14253=VERTEX_POINT ( 'NONE', #10275 ) ;
#14259=ORIENTED_EDGE ( 'NONE', *, *, #17270, .F. ) ;
#14262=VERTEX_POINT ( 'NONE', #10051 ) ;
#14264=CARTESIAN_POINT ( 'NONE',  ( 35.84667945578129888, -10.83917230622230043, -13.00000000000000000 ) ) ;
#14265=CARTESIAN_POINT ( 'NONE',  ( 43.66832999130209458, 21.22121844545429781, -13.00000000000000000 ) ) ;
#14276=LINE ( 'NONE', #21516, #10271 ) ;
#14280=EDGE_CURVE ( 'NONE', #21767, #15043, #1000, .T. ) ;
#14282=VECTOR ( 'NONE', #10296, 1000.000000000000227 ) ;
#14285=VECTOR ( 'NONE', #19059, 1000.000000000000227 ) ;
#14291=CARTESIAN_POINT ( 'NONE',  ( 113.9239269372040013, -8.791386740117969723, 3.438967838479089450E-14 ) ) ;
#14292=ORIENTED_EDGE ( 'NONE', *, *, #23344, .F. ) ;
#14301=VECTOR ( 'NONE', #15589, 1000.000000000000227 ) ;
#14305=CARTESIAN_POINT ( 'NONE',  ( 41.08211621068439712, 11.24883806106539907, -19.59999999999999787 ) ) ;
#14312=EDGE_CURVE ( 'NONE', #10583, #20142, #23004, .T. ) ;
#14324=AXIS2_PLACEMENT_3D ( 'NONE', #17627, #1330, #867 ) ;
#14330=LINE ( 'NONE', #21560, #21161 ) ;
#14335=AXIS2_PLACEMENT_3D ( 'NONE', #15272, #22155, #5897 ) ;
#14343=PLANE ( 'NONE',  #1460 ) ;
#14345=EDGE_CURVE ( 'NONE', #9613, #5079, #14396, .T. ) ;
#14346=VERTEX_POINT ( 'NONE', #23414 ) ;
#14352=CARTESIAN_POINT ( 'NONE',  ( 41.17437060284130013, 11.63805410277980101, 19.59999999999999787 ) ) ;
#14363=EDGE_CURVE ( 'NONE', #7703, #11043, #15945, .T. ) ;
#14364=FACE_OUTER_BOUND ( 'NONE', #15750, .T. ) ;
#14372=CARTESIAN_POINT ( 'NONE',  ( 117.1241794131700118, -12.63305097454420078, -15.50000000000000000 ) ) ;
#14388=DIRECTION ( 'NONE',  ( -0.9730401042858022320, 0.2306359803922080343, 5.959266323858941219E-17 ) ) ;
#14395=DIRECTION ( 'NONE',  ( -0.2306359803922078400, -0.9730401042858023430, 5.204170427930423650E-15 ) ) ;
#14396=LINE ( 'NONE', #17984, #16949 ) ;
#14405=ORIENTED_EDGE ( 'NONE', *, *, #14641, .T. ) ;
#14411=DIRECTION ( 'NONE',  ( -0.9730401042858023430, 0.2306359803922080620, 5.959266323858944916E-17 ) ) ;
#14413=CARTESIAN_POINT ( 'NONE',  ( 114.8178196092480050, -22.36345201740219935, 13.00000000000000000 ) ) ;
#14416=VECTOR ( 'NONE', #21629, 1000.000000000000227 ) ;
#14425=CARTESIAN_POINT ( 'NONE',  ( 50.76434296088209663, 17.41090750189739822, 3.560102062092729998E-14 ) ) ;
#14427=CARTESIAN_POINT ( 'NONE',  ( 50.90756547144185618, 18.01515514085710734, -2.066999999999964199 ) ) ;
#14431=CARTESIAN_POINT ( 'NONE',  ( 45.41807264205800010, 29.54199202163849947, -9.133960000000000079 ) ) ;
#14445=DIRECTION ( 'NONE',  ( -0.9730401042858024541, 0.2306359803922080898, 5.959266323858912869E-17 ) ) ;
#14456=DIRECTION ( 'NONE',  ( -0.5249589903860224505, 0.8511275218278915311, 1.187479569643817911E-16 ) ) ;
#14457=ORIENTED_EDGE ( 'NONE', *, *, #12759, .T. ) ;
#14486=CARTESIAN_POINT ( 'NONE',  ( 45.07211867146960316, 28.08243186520980217, -10.02499999999999858 ) ) ;
#14488=ORIENTED_EDGE ( 'NONE', *, *, #1114, .T. ) ;
#14490=VERTEX_POINT ( 'NONE', #9776 ) ;
#14493=DIRECTION ( 'NONE',  ( 0.9730401042858024541, -0.2306359803922080898, -5.959266323858942451E-17 ) ) ;
#14495=DIRECTION ( 'NONE',  ( 4.758660364968300250E-15, 2.033490192229560220E-14, -1.000000000000000000 ) ) ;
#14496=ORIENTED_EDGE ( 'NONE', *, *, #5431, .T. ) ;
#14512=CARTESIAN_POINT ( 'NONE',  ( 45.41807264205800010, 29.54199202163849947, 9.133960000000000079 ) ) ;
#14513=VECTOR ( 'NONE', #11099, 1000.000000000000000 ) ;
#14515=LINE ( 'NONE', #3938, #17851 ) ;
#14524=DIRECTION ( 'NONE',  ( -1.524428182562999945E-15, -6.173091865707990781E-15, -1.000000000000000000 ) ) ;
#14535=ORIENTED_EDGE ( 'NONE', *, *, #21135, .F. ) ;
#14539=CONICAL_SURFACE ( 'NONE', #7342, 2.283500000000000085, 0.7853981633974447263 ) ;
#14544=CARTESIAN_POINT ( 'NONE',  ( 114.8178196092480050, -22.36345201740219935, -20.00000000000000000 ) ) ;
#14548=LINE ( 'NONE', #16313, #9631 ) ;
#14557=CARTESIAN_POINT ( 'NONE',  ( 53.20239347634440463, 27.69690417850090114, 3.288194835581189691E-14 ) ) ;
#14575=DIRECTION ( 'NONE',  ( -0.9730401042858024541, 0.2306359803922080898, 5.959266323858942451E-17 ) ) ;
#14579=CARTESIAN_POINT ( 'NONE',  ( 117.1241794131700118, -12.63305097454420078, -15.50000000000000000 ) ) ;
#14630=EDGE_CURVE ( 'NONE', #12948, #3328, #7862, .T. ) ;
#14631=EDGE_LOOP ( 'NONE', ( #2704, #2664 ) ) ;
#14635=ORIENTED_EDGE ( 'NONE', *, *, #17547, .T. ) ;
#14641=EDGE_CURVE ( 'NONE', #7551, #16084, #9400, .T. ) ;
#14642=FACE_OUTER_BOUND ( 'NONE', #849, .T. ) ;
#14644=CARTESIAN_POINT ( 'NONE',  ( 46.46175228317039796, -6.161274394849590053, -13.00000000000000000 ) ) ;
#14649=VERTEX_POINT ( 'NONE', #11092 ) ;
#14653=CARTESIAN_POINT ( 'NONE',  ( 97.29330225143137056, -16.08541248458771022, 13.00000000000000000 ) ) ;
#14664=CARTESIAN_POINT ( 'NONE',  ( 113.2956221386590130, -28.78551670568859677, -2.700000000000000178 ) ) ;
#14669=DIRECTION ( 'NONE',  ( 0.9730401042858024541, -0.2306359803922080898, -5.959266323858852472E-17 ) ) ;
#14670=AXIS2_PLACEMENT_3D ( 'NONE', #5256, #7061, #3708 ) ;
#14683=ORIENTED_EDGE ( 'NONE', *, *, #15661, .F. ) ;
#14684=AXIS2_PLACEMENT_3D ( 'NONE', #11339, #9419, #9780 ) ;
#14689=CONICAL_SURFACE ( 'NONE', #11299, 2.283499999999998753, 0.7853981633974433940 ) ;
#14694=CARTESIAN_POINT ( 'NONE',  ( 114.2412296582679971, -24.79605227811670076, -2.999999999999940048 ) ) ;
#14698=ORIENTED_EDGE ( 'NONE', *, *, #17072, .F. ) ;
#14706=DIRECTION ( 'NONE',  ( 0.1177891644214619504, 0.4969457958705769118, 0.8597503060257977170 ) ) ;
#14713=DIRECTION ( 'NONE',  ( 0.2306359803922053142, 0.9730401042858028982, 0.000000000000000000 ) ) ;
#14715=EDGE_LOOP ( 'NONE', ( #18196, #11912, #10418, #286 ) ) ;
#14745=ADVANCED_BREP_SHAPE_REPRESENTATION ( '', ( #9171, #12739 ), #21598 ) ;
#14749=CARTESIAN_POINT ( 'NONE',  ( 114.2412296582679971, -24.79605227811670076, -2.999999999999940048 ) ) ;
#14755=CYLINDRICAL_SURFACE ( 'NONE', #18315, 7.000000000000000000 ) ;
#14758=VERTEX_POINT ( 'NONE', #8576 ) ;
#14762=DIRECTION ( 'NONE',  ( 0.2306359803922080620, 0.9730401042858023430, 5.073893018238513068E-14 ) ) ;
#14769=EDGE_CURVE ( 'NONE', #104, #9613, #2933, .T. ) ;
#14788=ORIENTED_EDGE ( 'NONE', *, *, #8240, .T. ) ;
#14792=ADVANCED_FACE ( 'NONE', ( #19368 ), #13670, .T. ) ;
#14799=CARTESIAN_POINT ( 'NONE',  ( 41.61257896558653613, 13.48683030092277235, 3.881831259975344606E-14 ) ) ;
#14801=ORIENTED_EDGE ( 'NONE', *, *, #10326, .T. ) ;
#14802=LINE ( 'NONE', #183, #18744 ) ;
#14807=VECTOR ( 'NONE', #8706, 1000.000000000000227 ) ;
#14808=DIRECTION ( 'NONE',  ( 0.000000000000000000, 0.000000000000000000, -1.000000000000000000 ) ) ;
#14809=CARTESIAN_POINT ( 'NONE',  ( 114.9405074087380001, 12.84085624101770051, 2.283500000000028951 ) ) ;
#14810=LINE ( 'NONE', #7458, #8015 ) ;
#14815=VERTEX_POINT ( 'NONE', #10369 ) ;
#14819=ORIENTED_EDGE ( 'NONE', *, *, #20444, .F. ) ;
#14825=DIRECTION ( 'NONE',  ( -0.9730401042858024541, 0.2306359803922080898, 5.959266323858942451E-17 ) ) ;
#14831=ORIENTED_EDGE ( 'NONE', *, *, #19681, .T. ) ;
#14838=VERTEX_POINT ( 'NONE', #2979 ) ;
#14872=DIRECTION ( 'NONE',  ( 0.9730401042858024541, -0.2306359803922080898, -5.959266323858942451E-17 ) ) ;
#14876=AXIS2_PLACEMENT_3D ( 'NONE', #15455, #12151, #12276 ) ;
#14881=VERTEX_POINT ( 'NONE', #19493 ) ;
#14882=CARTESIAN_POINT ( 'NONE',  ( 114.2412296582679971, -24.79605227811680379, 3.000000000000000000 ) ) ;
#14908=EDGE_CURVE ( 'NONE', #2588, #1063, #5467, .T. ) ;
#14914=EDGE_LOOP ( 'NONE', ( #214, #18768, #20947, #4377 ) ) ;
#14929=AXIS2_PLACEMENT_3D ( 'NONE', #5078, #4830, #16107 ) ;
#14930=CARTESIAN_POINT ( 'NONE',  ( 118.5079952955230027, -6.794810348829359192, -15.50000000000000000 ) ) ;
#14959=ORIENTED_EDGE ( 'NONE', *, *, #16481, .F. ) ;
#14962=DIRECTION ( 'NONE',  ( 0.000000000000000000, 0.000000000000000000, 1.000000000000000000 ) ) ;
#14968=ORIENTED_EDGE ( 'NONE', *, *, #4675, .T. ) ;
#14983=ORIENTED_EDGE ( 'NONE', *, *, #23434, .F. ) ;
#14986=EDGE_LOOP ( 'NONE', ( #6847, #4863, #1051, #6046 ) ) ;
#14987=DIRECTION ( 'NONE',  ( 1.000000000000000000, -1.176672321210050136E-14, 0.000000000000000000 ) ) ;
#14996=DIRECTION ( 'NONE',  ( -0.2306359803922080343, -0.9730401042858022320, 1.015202274805050187E-13 ) ) ;
#15006=EDGE_CURVE ( 'NONE', #7688, #23458, #19952, .T. ) ;
#15018=CARTESIAN_POINT ( 'NONE',  ( 120.3930287342899987, 3.035456073538489896, 13.00000000000000000 ) ) ;
#15024=DIRECTION ( 'NONE',  ( 0.9730401042858024541, -0.2306359803922080898, -5.959266323858942451E-17 ) ) ;
#15037=DIRECTION ( 'NONE',  ( -0.9730401042858022320, 0.2306359803922080343, 5.959266323858941219E-17 ) ) ;
#15042=DIRECTION ( 'NONE',  ( -0.2306359803922053697, -0.9730401042858028982, 0.000000000000000000 ) ) ;
#15043=VERTEX_POINT ( 'NONE', #17716 ) ;
#15054=DIRECTION ( 'NONE',  ( -0.9730401042858024541, 0.2306359803922080898, 5.959266323858942451E-17 ) ) ;
#15057=ORIENTED_EDGE ( 'NONE', *, *, #21538, .T. ) ;
#15072=DIRECTION ( 'NONE',  ( 0.2306359803922080898, 0.9730401042858024541, -2.572202231434325988E-16 ) ) ;
#15073=VERTEX_POINT ( 'NONE', #16605 ) ;
#15083=AXIS2_PLACEMENT_3D ( 'NONE', #1006, #6982, #15629 ) ;
#15087=AXIS2_PLACEMENT_3D ( 'NONE', #3620, #10777, #1715 ) ;
#15089=DIRECTION ( 'NONE',  ( -0.2306359803922080620, -0.9730401042858023430, 5.397021885244292808E-15 ) ) ;
#15091=EDGE_CURVE ( 'NONE', #11874, #21452, #11061, .T. ) ;
#15096=LINE ( 'NONE', #7618, #10955 ) ;
#15098=AXIS2_PLACEMENT_3D ( 'NONE', #1794, #10505, #16407 ) ;
#15105=ORIENTED_EDGE ( 'NONE', *, *, #1114, .F. ) ;
#15110=DIRECTION ( 'NONE',  ( 0.2306359803922077290, 0.9730401042858024541, -1.412237191019971018E-17 ) ) ;
#15118=PLANE ( 'NONE',  #21745 ) ;
#15137=ORIENTED_EDGE ( 'NONE', *, *, #20798, .F. ) ;
#15138=LINE ( 'NONE', #2322, #10945 ) ;
#15144=ORIENTED_EDGE ( 'NONE', *, *, #3425, .F. ) ;
#15163=ADVANCED_FACE ( 'NONE', ( #22189 ), #9500, .F. ) ;
#15174=DIRECTION ( 'NONE',  ( -0.9730401042858024541, 0.2306359803922080898, 5.959266323858942451E-17 ) ) ;
#15178=ORIENTED_EDGE ( 'NONE', *, *, #3410, .F. ) ;
#15188=EDGE_LOOP ( 'NONE', ( #1080, #22842, #2796, #9282 ) ) ;
#15189=DIRECTION ( 'NONE',  ( 0.2306359803922076457, 0.9730401042858025651, 0.000000000000000000 ) ) ;
#15195=ORIENTED_EDGE ( 'NONE', *, *, #20585, .F. ) ;
#15201=VERTEX_POINT ( 'NONE', #21839 ) ;
#15202=LINE ( 'NONE', #22443, #12298 ) ;
#15213=CYLINDRICAL_SURFACE ( 'NONE', #11737, 2.999999999999999556 ) ;
#15216=ORIENTED_EDGE ( 'NONE', *, *, #23114, .T. ) ;
#15217=CARTESIAN_POINT ( 'NONE',  ( 113.9197686726213448, -24.27486053345101169, -13.00000000000000000 ) ) ;
#15231=ADVANCED_FACE ( 'NONE', ( #15666 ), #11895, .T. ) ;
#15233=CARTESIAN_POINT ( 'NONE',  ( 120.8143550994449953, 2.935590694028619829, -13.00000000000000000 ) ) ;
#15237=FACE_OUTER_BOUND ( 'NONE', #6167, .T. ) ;
#15252=CIRCLE ( 'NONE', #16010, 0.3999999999999998557 ) ;
#15259=ORIENTED_EDGE ( 'NONE', *, *, #4735, .T. ) ;
#15272=CARTESIAN_POINT ( 'NONE',  ( 37.88245768368250310, -4.127756955731490152, 13.00000000000000000 ) ) ;
#15283=CARTESIAN_POINT ( 'NONE',  ( 115.1780992045983680, -12.17177901375979410, 3.431286017404439083E-14 ) ) ;
#15303=CARTESIAN_POINT ( 'NONE',  ( 122.4288069621910040, 9.746871424029270869, 10.02499999999999858 ) ) ;
#15340=CARTESIAN_POINT ( 'NONE',  ( 114.1489752661110089, -25.18526831983109915, -3.000000000000000000 ) ) ;
#15365=LINE ( 'NONE', #10162, #14285 ) ;
#15366=DIRECTION ( 'NONE',  ( -1.164423685541410132E-14, -4.938475812832940103E-14, 1.000000000000000000 ) ) ;
#15371=CIRCLE ( 'NONE', #9311, 7.000000000000000000 ) ;
#15374=CARTESIAN_POINT ( 'NONE',  ( 114.9904400984930106, 13.05151942359559847, 2.909781424016149503E-14 ) ) ;
#15393=CARTESIAN_POINT ( 'NONE',  ( 112.4091670724712060, 2.161275108032480130, 3.197661755011519713E-14 ) ) ;
#15402=EDGE_LOOP ( 'NONE', ( #18899, #18844, #12569, #20220 ) ) ;
#15412=AXIS2_PLACEMENT_3D ( 'NONE', #12178, #11827, #15482 ) ;
#15419=EDGE_CURVE ( 'NONE', #18309, #15573, #10573, .T. ) ;
#15420=DIRECTION ( 'NONE',  ( 6.124378941434239724E-17, -2.274246353359159970E-33, 1.000000000000000000 ) ) ;
#15429=ORIENTED_EDGE ( 'NONE', *, *, #1133, .T. ) ;
#15435=EDGE_CURVE ( 'NONE', #2588, #9648, #17892, .T. ) ;
#15447=ORIENTED_EDGE ( 'NONE', *, *, #13329, .T. ) ;
#15449=EDGE_CURVE ( 'NONE', #11681, #12948, #4992, .T. ) ;
#15455=CARTESIAN_POINT ( 'NONE',  ( 117.8160873543469904, -9.713930661686799084, 3.415130773183659557E-14 ) ) ;
#15464=VECTOR ( 'NONE', #8890, 1000.000000000000000 ) ;
#15477=CARTESIAN_POINT ( 'NONE',  ( 114.0804991654443796, -24.53545640578393261, -13.00000000000000000 ) ) ;
#15482=DIRECTION ( 'NONE',  ( -0.2306359803922077290, -0.9730401042858024541, 0.000000000000000000 ) ) ;
#15483=EDGE_CURVE ( 'NONE', #1999, #3328, #20528, .T. ) ;
#15492=FACE_OUTER_BOUND ( 'NONE', #23118, .T. ) ;
#15498=DIRECTION ( 'NONE',  ( 6.124378941434239724E-17, -2.274246353359159970E-33, 1.000000000000000000 ) ) ;
#15500=LINE ( 'NONE', #8382, #14282 ) ;
#15503=FACE_OUTER_BOUND ( 'NONE', #19294, .T. ) ;
#15510=ADVANCED_FACE ( 'NONE', ( #21358 ), #21692, .T. ) ;
#15548=AXIS2_PLACEMENT_3D ( 'NONE', #19854, #10844, #1776 ) ;
#15556=CARTESIAN_POINT ( 'NONE',  ( 40.45939906362549721, 8.621629779493760637, 3.888892445930440142E-14 ) ) ;
#15562=DIRECTION ( 'NONE',  ( -0.9730401042858022320, 0.2306359803922080343, 5.959266323858941219E-17 ) ) ;
#15568=ORIENTED_EDGE ( 'NONE', *, *, #16966, .T. ) ;
#15570=DIRECTION ( 'NONE',  ( 0.2306359803922080898, 0.9730401042858024541, -2.572202231434325988E-16 ) ) ;
#15573=VERTEX_POINT ( 'NONE', #22042 ) ;
#15577=ORIENTED_EDGE ( 'NONE', *, *, #11122, .T. ) ;
#15578=ORIENTED_EDGE ( 'NONE', *, *, #22563, .F. ) ;
#15579=DIRECTION ( 'NONE',  ( -0.2306359803922080898, -0.9730401042858024541, 2.572202231434325988E-16 ) ) ;
#15584=CARTESIAN_POINT ( 'NONE',  ( 122.4288069621910040, 9.746871424029281528, -13.00000000000000000 ) ) ;
#15587=DIRECTION ( 'NONE',  ( 0.9730401042858024541, -0.2306359803922080898, -5.959266323858942451E-17 ) ) ;
#15589=DIRECTION ( 'NONE',  ( 0.2306359803922080343, 0.9730401042858022320, -2.572202231434325495E-16 ) ) ;
#15610=DIRECTION ( 'NONE',  ( -0.2306359803922080898, -0.9730401042858024541, 2.572202231434325988E-16 ) ) ;
#15611=EDGE_LOOP ( 'NONE', ( #9758, #9192, #8213, #4927 ) ) ;
#15615=CYLINDRICAL_SURFACE ( 'NONE', #12527, 0.3999999999999982458 ) ;
#15629=DIRECTION ( 'NONE',  ( -4.536707686694059956E-14, 1.228149275973191858E-30, -1.000000000000000000 ) ) ;
#15635=VERTEX_POINT ( 'NONE', #79 ) ;
#15637=DIRECTION ( 'NONE',  ( 0.9730401042858024541, -0.2306359803922080898, -5.959266323858942451E-17 ) ) ;
#15641=DIRECTION ( 'NONE',  ( -0.2306359803922081175, -0.9730401042858022320, 1.412237191019896138E-17 ) ) ;
#15644=VERTEX_POINT ( 'NONE', #18270 ) ;
#15659=CARTESIAN_POINT ( 'NONE',  ( 117.1933702072879981, -12.34113894325840022, 18.89999999999999858 ) ) ;
#15661=EDGE_CURVE ( 'NONE', #15073, #21187, #8441, .T. ) ;
#15666=FACE_OUTER_BOUND ( 'NONE', #4754, .T. ) ;
#15679=CIRCLE ( 'NONE', #21730, 2.066999999999999726 ) ;
#15692=CARTESIAN_POINT ( 'NONE',  ( 117.1241794131700118, -12.63305097454420078, 15.50000000000000000 ) ) ;
#15702=DIRECTION ( 'NONE',  ( -0.8511275218278966381, -0.5249589903860140128, 5.212440122911323074E-17 ) ) ;
#15706=EDGE_CURVE ( 'NONE', #19560, #2719, #11170, .T. ) ;
#15712=FACE_OUTER_BOUND ( 'NONE', #4217, .T. ) ;
#15716=CARTESIAN_POINT ( 'NONE',  ( 36.10037903421270755, -9.768828191507939351, 3.399999999999999911 ) ) ;
#15717=CARTESIAN_POINT ( 'NONE',  ( 113.9239269372040013, -8.791386740117969723, 3.438967838479089450E-14 ) ) ;
#15721=FACE_OUTER_BOUND ( 'NONE', #2468, .T. ) ;
#15722=LINE ( 'NONE', #4792, #3301 ) ;
#15723=PLANE ( 'NONE',  #12403 ) ;
#15724=LINE ( 'NONE', #22953, #10919 ) ;
#15733=DIRECTION ( 'NONE',  ( -0.9730401042858023430, 0.2306359803922080620, 5.959266323858944916E-17 ) ) ;
#15738=DIRECTION ( 'NONE',  ( -0.9730401042858024541, 0.2306359803922080898, 5.959266323858723049E-17 ) ) ;
#15750=EDGE_LOOP ( 'NONE', ( #17326, #915, #22081, #6383, #5794, #19730, #2731, #2384, #18499, #20426, #18856, #15178, #19613, #21268, #15876, #21366, #5587, #6991, #1896, #14034, #8846, #2267, #7692, #5183, #20074, #22142, #20987, #13858, #15195, #21114, #21068, #22888, #19672, #6133, #7617, #1885, #8298, #883, #4664, #20325, #20306, #11139, #5614, #17980, #16730, #21224, #689, #17780 ) ) ;
#15752=AXIS2_PLACEMENT_3D ( 'NONE', #6809, #19945, #19394 ) ;
#15766=ORIENTED_EDGE ( 'NONE', *, *, #10118, .T. ) ;
#15772=CIRCLE ( 'NONE', #953, 7.000000000000000888 ) ;
#15776=DIRECTION ( 'NONE',  ( -0.9730401042858022320, 0.2306359803922080343, 5.959266323858941219E-17 ) ) ;
#15779=DIRECTION ( 'NONE',  ( 0.2306359803922080343, 0.9730401042858022320, -2.572202231434325495E-16 ) ) ;
#15792=CIRCLE ( 'NONE', #9342, 4.999999999999998224 ) ;
#15794=ORIENTED_EDGE ( 'NONE', *, *, #22919, .F. ) ;
#15795=DIRECTION ( 'NONE',  ( -0.9730401042858022320, 0.2306359803922080343, 5.959266323858941219E-17 ) ) ;
#15799=DIRECTION ( 'NONE',  ( -0.9730401042858024541, 0.2306359803922080898, 5.959266323858942451E-17 ) ) ;
#15808=EDGE_CURVE ( 'NONE', #4850, #4506, #17508, .T. ) ;
#15810=CARTESIAN_POINT ( 'NONE',  ( 38.19845176233020823, -1.855887187839940777, 13.00000000000000000 ) ) ;
#15812=VERTEX_POINT ( 'NONE', #19180 ) ;
#15825=FACE_OUTER_BOUND ( 'NONE', #3279, .T. ) ;
#15831=VERTEX_POINT ( 'NONE', #11829 ) ;
#15841=ORIENTED_EDGE ( 'NONE', *, *, #18634, .T. ) ;
#15849=DIRECTION ( 'NONE',  ( -0.9730401042858022320, 0.2306359803922080343, 5.959266323858941219E-17 ) ) ;
#15863=PLANE ( 'NONE',  #9928 ) ;
#15864=VECTOR ( 'NONE', #3943, 1000.000000000000227 ) ;
#15865=VERTEX_POINT ( 'NONE', #3135 ) ;
#15869=EDGE_LOOP ( 'NONE', ( #4861, #7819, #5324, #3103 ) ) ;
#15876=ORIENTED_EDGE ( 'NONE', *, *, #10661, .F. ) ;
#15877=CARTESIAN_POINT ( 'NONE',  ( 39.74442752440959481, 5.605205456207790427, -19.59999999999999787 ) ) ;
#15880=AXIS2_PLACEMENT_3D ( 'NONE', #17248, #17114, #6308 ) ;
#15884=EDGE_LOOP ( 'NONE', ( #4654, #20953, #6212, #20445 ) ) ;
#15895=ORIENTED_EDGE ( 'NONE', *, *, #16465, .T. ) ;
#15909=DIRECTION ( 'NONE',  ( 6.124378941434239724E-17, -2.274246353359159970E-33, 1.000000000000000000 ) ) ;
#15929=DIRECTION ( 'NONE',  ( 0.2306359803922053142, 0.9730401042858028982, 0.000000000000000000 ) ) ;
#15933=DIRECTION ( 'NONE',  ( -0.2306359803922080343, -0.9730401042858022320, -7.611545645953073104E-14 ) ) ;
#15935=CARTESIAN_POINT ( 'NONE',  ( 113.2033677465029911, -29.17473274740279976, 3.100000000000039613 ) ) ;
#15942=ADVANCED_FACE ( 'NONE', ( #10756 ), #11494, .F. ) ;
#15943=VECTOR ( 'NONE', #3349, 1000.000000000000227 ) ;
#15945=LINE ( 'NONE', #9177, #4441 ) ;
#15948=DIRECTION ( 'NONE',  ( -0.2306359803922054252, -0.9730401042858028982, 0.000000000000000000 ) ) ;
#15960=CIRCLE ( 'NONE', #22017, 2.066999999999998394 ) ;
#15976=DIRECTION ( 'NONE',  ( -0.8511275218278966381, -0.5249589903860140128, 5.212440122911323074E-17 ) ) ;
#15990=AXIS2_PLACEMENT_3D ( 'NONE', #22939, #8588, #8703 ) ;
#16008=ORIENTED_EDGE ( 'NONE', *, *, #14312, .T. ) ;
#16009=VECTOR ( 'NONE', #18809, 1000.000000000000227 ) ;
#16010=AXIS2_PLACEMENT_3D ( 'NONE', #1901, #16053, #19733 ) ;
#16028=ADVANCED_FACE ( 'NONE', ( #14642 ), #1921, .F. ) ;
#16036=VERTEX_POINT ( 'NONE', #3822 ) ;
#16041=CARTESIAN_POINT ( 'NONE',  ( 113.8430260960419957, 8.210644904773758412, 2.067000000000030369 ) ) ;
#16053=DIRECTION ( 'NONE',  ( -0.9730401042858024541, 0.2306359803922080898, 5.959266323858232476E-17 ) ) ;
#16084=VERTEX_POINT ( 'NONE', #22464 ) ;
#16095=DIRECTION ( 'NONE',  ( 0.2306359803922080620, 0.9730401042858023430, 1.268685090138121373E-13 ) ) ;
#16098=CARTESIAN_POINT ( 'NONE',  ( 120.8143550994449953, 2.935590694028619829, -20.00000000000000000 ) ) ;
#16100=DIRECTION ( 'NONE',  ( -0.9730401042858022320, 0.2306359803922080343, 5.959266323858941219E-17 ) ) ;
#16103=VERTEX_POINT ( 'NONE', #20685 ) ;
#16106=ORIENTED_EDGE ( 'NONE', *, *, #684, .T. ) ;
#16107=DIRECTION ( 'NONE',  ( -0.2306359803921919083, -0.9730401042858062288, 2.222614453595293935E-13 ) ) ;
#16110=VERTEX_POINT ( 'NONE', #17003 ) ;
#16118=CARTESIAN_POINT ( 'NONE',  ( 120.8143550994449953, 2.935590694028619829, -13.00000000000000000 ) ) ;
#16123=EDGE_CURVE ( 'NONE', #4401, #7703, #20451, .T. ) ;
#16125=DIRECTION ( 'NONE',  ( -1.000000000000000000, -1.869969807519020344E-43, -1.749697687228930073E-14 ) ) ;
#16126=FACE_OUTER_BOUND ( 'NONE', #10605, .T. ) ;
#16129=CARTESIAN_POINT ( 'NONE',  ( 42.88107685774368605, 18.83855087449469679, 13.00000000000000000 ) ) ;
#16132=ORIENTED_EDGE ( 'NONE', *, *, #6334, .T. ) ;
#16157=CARTESIAN_POINT ( 'NONE',  ( 115.1338136878955964, -20.09158224951067240, 13.00000000000000000 ) ) ;
#16164=CARTESIAN_POINT ( 'NONE',  ( 114.9904400984930106, 13.05151942359559847, 2.909781424016149503E-14 ) ) ;
#16171=VECTOR ( 'NONE', #17087, 1000.000000000000227 ) ;
#16175=LINE ( 'NONE', #3596, #4868 ) ;
#16185=AXIS2_PLACEMENT_3D ( 'NONE', #10463, #14231, #8659 ) ;
#16187=DIRECTION ( 'NONE',  ( 0.000000000000000000, -4.196234823359475661E-16, -1.000000000000000000 ) ) ;
#16196=CARTESIAN_POINT ( 'NONE',  ( 102.2474456857739966, -6.023754975411469204, 3.510479034365399954E-14 ) ) ;
#16209=CIRCLE ( 'NONE', #2171, 2.499999999999999112 ) ;
#16215=AXIS2_PLACEMENT_3D ( 'NONE', #7652, #14493, #9148 ) ;
#16218=EDGE_CURVE ( 'NONE', #9054, #15865, #7867, .T. ) ;
#16219=EDGE_CURVE ( 'NONE', #23127, #17030, #7989, .T. ) ;
#16229=ORIENTED_EDGE ( 'NONE', *, *, #17270, .T. ) ;
#16241=LINE ( 'NONE', #23354, #19593 ) ;
#16246=ADVANCED_FACE ( 'NONE', ( #22685 ), #11114, .F. ) ;
#16258=CARTESIAN_POINT ( 'NONE',  ( 53.15246078658950069, 27.48624099592299785, -2.283499999999966779 ) ) ;
#16281=DIRECTION ( 'NONE',  ( 0.1630842657209384816, 0.6880432561069583786, -0.7071067811865453523 ) ) ;
#16305=EDGE_CURVE ( 'NONE', #21743, #18309, #12274, .T. ) ;
#16313=CARTESIAN_POINT ( 'NONE',  ( 36.10037903421270755, -9.768828191507928693, 2.700000000000049916 ) ) ;
#16314=EDGE_CURVE ( 'NONE', #19758, #16103, #20954, .T. ) ;
#16315=EDGE_CURVE ( 'NONE', #2314, #12703, #4659, .T. ) ;
#16324=DIRECTION ( 'NONE',  ( 0.2306359803922080898, 0.9730401042858024541, -2.572202231434325988E-16 ) ) ;
#16334=EDGE_LOOP ( 'NONE', ( #15577, #14405 ) ) ;
#16381=ORIENTED_EDGE ( 'NONE', *, *, #19122, .T. ) ;
#16385=CARTESIAN_POINT ( 'NONE',  ( 37.67179450110460692, -4.077824265976569329, -13.00000000000000000 ) ) ;
#16389=VERTEX_POINT ( 'NONE', #17958 ) ;
#16396=CARTESIAN_POINT ( 'NONE',  ( 120.8143550994449953, 2.935590694028659797, 13.00000000000000000 ) ) ;
#16407=DIRECTION ( 'NONE',  ( -1.000000000000000000, 0.000000000000000000, 6.124317834331790129E-17 ) ) ;
#16409=ORIENTED_EDGE ( 'NONE', *, *, #9954, .F. ) ;
#16415=CARTESIAN_POINT ( 'NONE',  ( 112.5523895830310011, 2.765522746992189695, 3.181688650527689809E-14 ) ) ;
#16434=DIRECTION ( 'NONE',  ( 0.2306359803922080898, 0.9730401042858024541, -2.572202231434325988E-16 ) ) ;
#16449=VERTEX_POINT ( 'NONE', #10723 ) ;
#16465=EDGE_CURVE ( 'NONE', #5109, #21047, #18062, .T. ) ;
#16481=EDGE_CURVE ( 'NONE', #14815, #16110, #1772, .T. ) ;
#16489=CYLINDRICAL_SURFACE ( 'NONE', #6193, 2.066999999999997950 ) ;
#16491=EDGE_CURVE ( 'NONE', #13288, #2314, #5772, .T. ) ;
#16500=ORIENTED_EDGE ( 'NONE', *, *, #8807, .F. ) ;
#16522=CYLINDRICAL_SURFACE ( 'NONE', #4797, 0.4000000000000010214 ) ;
#16525=DIRECTION ( 'NONE',  ( -0.9730401042858023430, 0.2306359803922080620, 5.959266323858944916E-17 ) ) ;
#16528=ADVANCED_FACE ( 'NONE', ( #19723 ), #14539, .F. ) ;
#16538=CARTESIAN_POINT ( 'NONE',  ( 114.0804991654443796, -24.53545640578393261, 13.00000000000000000 ) ) ;
#16541=DIRECTION ( 'NONE',  ( -0.9730401042858024541, 0.2306359803922080898, 5.959266323858942451E-17 ) ) ;
#16549=DIRECTION ( 'NONE',  ( 0.000000000000000000, 0.000000000000000000, 1.000000000000000000 ) ) ;
#16557=ORIENTED_EDGE ( 'NONE', *, *, #22563, .T. ) ;
#16559=ORIENTED_EDGE ( 'NONE', *, *, #3594, .F. ) ;
#16560=AXIS2_PLACEMENT_3D ( 'NONE', #9957, #13505, #9835 ) ;
#16569=CARTESIAN_POINT ( 'NONE',  ( 122.4288069621910040, 9.746871424029270869, 10.02499999999999858 ) ) ;
#16573=CIRCLE ( 'NONE', #20759, 0.3999999999999982458 ) ;
#16592=AXIS2_PLACEMENT_3D ( 'NONE', #18474, #2185, #9441 ) ;
#16599=LINE ( 'NONE', #20186, #18318 ) ;
#16605=CARTESIAN_POINT ( 'NONE',  ( 38.35918225515318625, -2.116483060172758446, 13.00000000000000000 ) ) ;
#16614=ORIENTED_EDGE ( 'NONE', *, *, #17547, .F. ) ;
#16615=ORIENTED_EDGE ( 'NONE', *, *, #14190, .T. ) ;
#16621=DIRECTION ( 'NONE',  ( 6.124378941434239724E-17, -2.274246353359159970E-33, 1.000000000000000000 ) ) ;
#16635=DIRECTION ( 'NONE',  ( -0.9730401042858024541, 0.2306359803922080898, 5.959266323863401980E-17 ) ) ;
#16639=DIRECTION ( 'NONE',  ( -0.9730401042858024541, 0.2306359803922080898, 5.959266323858723049E-17 ) ) ;
#16654=DIRECTION ( 'NONE',  ( -0.9730401042858023430, 0.2306359803922080620, 5.959266323858944916E-17 ) ) ;
#16656=CARTESIAN_POINT ( 'NONE',  ( 97.29330225143137056, -16.08541248458771022, -13.00000000000000000 ) ) ;
#16666=DIRECTION ( 'NONE',  ( 0.000000000000000000, 0.000000000000000000, 1.000000000000000000 ) ) ;
#16671=ORIENTED_EDGE ( 'NONE', *, *, #5781, .T. ) ;
#16675=DIRECTION ( 'NONE',  ( -0.9730401042858022320, 0.2306359803922080343, 5.959266323858941219E-17 ) ) ;
#16680=PRODUCT_DEFINITION_FORMATION_WITH_SPECIFIED_SOURCE ( 'ANY', '', #1697, .NOT_KNOWN. ) ;
#16696=CARTESIAN_POINT ( 'NONE',  ( 43.40226860240920814, 19.16001186014064572, -13.00000000000000000 ) ) ;
#16702=DIRECTION ( 'NONE',  ( -0.9730401042858024541, 0.2306359803922080898, 5.959266323858942451E-17 ) ) ;
#16730=ORIENTED_EDGE ( 'NONE', *, *, #18858, .F. ) ;
#16754=ORIENTED_EDGE ( 'NONE', *, *, #19162, .F. ) ;
#16760=CYLINDRICAL_SURFACE ( 'NONE', #1773, 12.49999999999999645 ) ;
#16766=DIRECTION ( 'NONE',  ( 0.2306359803922095053, 0.9730401042858018990, 0.000000000000000000 ) ) ;
#16768=CIRCLE ( 'NONE', #22837, 2.499999999999999112 ) ;
#16779=PLANE ( 'NONE',  #6966 ) ;
#16786=DIRECTION ( 'NONE',  ( 0.2306359803922085339, 0.9730401042858022320, 0.000000000000000000 ) ) ;
#16787=AXIS2_PLACEMENT_3D ( 'NONE', #9812, #8147, #20718 ) ;
#16788=CIRCLE ( 'NONE', #17167, 0.3999999999999982458 ) ;
#16796=AXIS2_PLACEMENT_3D ( 'NONE', #19833, #20054, #14713 ) ;
#16808=DIRECTION ( 'NONE',  ( -0.9730401042858022320, 0.2306359803922080343, 5.959266323858941219E-17 ) ) ;
#16812=DIRECTION ( 'NONE',  ( 1.164423685541410132E-14, 4.938475812832940103E-14, -1.000000000000000000 ) ) ;
#16815=CARTESIAN_POINT ( 'NONE',  ( 106.2939232160746883, -18.21879530321555052, 13.00000000000000000 ) ) ;
#16822=CIRCLE ( 'NONE', #18344, 0.3999999999999982458 ) ;
#16829=DIRECTION ( 'NONE',  ( -0.9730401042858022320, 0.2306359803922080343, 5.959266323858941219E-17 ) ) ;
#16830=EDGE_LOOP ( 'NONE', ( #20382, #17925, #23311, #6131 ) ) ;
#16852=ORIENTED_EDGE ( 'NONE', *, *, #20712, .T. ) ;
#16854=ORIENTED_EDGE ( 'NONE', *, *, #6029, .T. ) ;
#16874=CARTESIAN_POINT ( 'NONE',  ( 117.1011158151309957, -12.73035498497280038, 20.00000000000000000 ) ) ;
#16878=CARTESIAN_POINT ( 'NONE',  ( 114.8178196092480050, -22.36345201740219935, -20.00000000000000000 ) ) ;
#16883=DIRECTION ( 'NONE',  ( -0.9730401042858024541, 0.2306359803922080898, 5.959266323858952312E-17 ) ) ;
#16885=EDGE_LOOP ( 'NONE', ( #2033, #4070, #11029, #19514 ) ) ;
#16886=PLANE ( 'NONE',  #3504 ) ;
#16897=AXIS2_PLACEMENT_3D ( 'NONE', #23348, #14575, #7106 ) ;
#16900=FACE_OUTER_BOUND ( 'NONE', #14002, .T. ) ;
#16903=CARTESIAN_POINT ( 'NONE',  ( 60.98218416654080443, 14.99311160239464336, 13.00000000000000000 ) ) ;
#16905=LINE ( 'NONE', #5746, #5982 ) ;
#16912=CARTESIAN_POINT ( 'NONE',  ( 118.4388045014059969, -7.086722380115130449, 18.89999999999999858 ) ) ;
#16915=CARTESIAN_POINT ( 'NONE',  ( 117.0319250210129951, -13.02226701625859917, 15.90000000000000036 ) ) ;
#16917=AXIS2_PLACEMENT_3D ( 'NONE', #19016, #11918, #7852 ) ;
#16919=DIRECTION ( 'NONE',  ( 5.401314170743249993E-15, 2.304622183485879988E-14, -1.000000000000000000 ) ) ;
#16928=AXIS2_PLACEMENT_3D ( 'NONE', #18188, #12844, #19737 ) ;
#16940=CARTESIAN_POINT ( 'NONE',  ( 118.5310588935630136, -6.697506338400819992, 20.00000000000000000 ) ) ;
#16949=VECTOR ( 'NONE', #12400, 1000.000000000000227 ) ;
#16959=CIRCLE ( 'NONE', #21131, 7.000000000000000888 ) ;
#16963=AXIS2_PLACEMENT_3D ( 'NONE', #4766, #18912, #6791 ) ;
#16966=EDGE_CURVE ( 'NONE', #6033, #171, #17183, .T. ) ;
#16975=CIRCLE ( 'NONE', #16215, 2.066999999999999726 ) ;
#16976=ORIENTED_EDGE ( 'NONE', *, *, #4410, .T. ) ;
#16984=ORIENTED_EDGE ( 'NONE', *, *, #11287, .T. ) ;
#16985=DIRECTION ( 'NONE',  ( -0.9730401042858022320, 0.2306359803922080343, 5.959266323858941219E-17 ) ) ;
#16990=CIRCLE ( 'NONE', #11328, 7.000000000000000000 ) ;
#16997=ORIENTED_EDGE ( 'NONE', *, *, #16315, .F. ) ;
#16999=DIRECTION ( 'NONE',  ( -0.9730401042858022320, 0.2306359803922080343, 5.959266323858941219E-17 ) ) ;
#17002=DIRECTION ( 'NONE',  ( -0.9730401042858022320, 0.2306359803922080343, 5.959266323858941219E-17 ) ) ;
#17003=CARTESIAN_POINT ( 'NONE',  ( 122.4288069621910040, 9.746871424029281528, -13.00000000000000000 ) ) ;
#17004=ORIENTED_EDGE ( 'NONE', *, *, #15435, .F. ) ;
#17030=VERTEX_POINT ( 'NONE', #16129 ) ;
#17032=DIRECTION ( 'NONE',  ( 0.000000000000000000, 0.000000000000000000, 1.000000000000000000 ) ) ;
#17039=DIRECTION ( 'NONE',  ( 0.9730401042858024541, -0.2306359803922080898, -5.959266323858942451E-17 ) ) ;
#17043=EDGE_CURVE ( 'NONE', #23363, #5959, #19933, .T. ) ;
#17051=DIRECTION ( 'NONE',  ( -0.8511275218278966381, -0.5249589903860140128, 5.212440122911323074E-17 ) ) ;
#17057=LINE ( 'NONE', #15283, #8775 ) ;
#17058=ORIENTED_EDGE ( 'NONE', *, *, #10006, .T. ) ;
#17072=EDGE_CURVE ( 'NONE', #13995, #5198, #22015, .T. ) ;
#17077=CONICAL_SURFACE ( 'NONE', #3792, 2.283499999999998753, 0.7853981633974433940 ) ;
#17078=AXIS2_PLACEMENT_3D ( 'NONE', #7615, #3697, #16621 ) ;
#17087=DIRECTION ( 'NONE',  ( -0.9730401042858022320, 0.2306359803922080343, 5.959266323858941219E-17 ) ) ;
#17096=EDGE_LOOP ( 'NONE', ( #9501, #20024 ) ) ;
#17103=LINE ( 'NONE', #22203, #12986 ) ;
#17114=DIRECTION ( 'NONE',  ( -0.9730401042858024541, 0.2306359803922080898, 5.959266323858942451E-17 ) ) ;
#17125=LINE ( 'NONE', #11342, #16009 ) ;
#17146=VECTOR ( 'NONE', #6635, 1000.000000000000227 ) ;
#17162=ORIENTED_EDGE ( 'NONE', *, *, #5888, .F. ) ;
#17166=ORIENTED_EDGE ( 'NONE', *, *, #17800, .F. ) ;
#17167=AXIS2_PLACEMENT_3D ( 'NONE', #10523, #4926, #12190 ) ;
#17168=PLANE ( 'NONE',  #21597 ) ;
#17179=EDGE_CURVE ( 'NONE', #8503, #2209, #17885, .T. ) ;
#17182=DIRECTION ( 'NONE',  ( 0.2306359803922080343, 0.9730401042858022320, 1.780177465867830349E-15 ) ) ;
#17183=CIRCLE ( 'NONE', #22098, 0.3999999999999998557 ) ;
#17184=EDGE_LOOP ( 'NONE', ( #8189, #20691, #14683, #19353 ) ) ;
#17188=AXIS2_PLACEMENT_3D ( 'NONE', #16196, #14411, #2532 ) ;
#17207=DIRECTION ( 'NONE',  ( 0.9730401042858024541, -0.2306359803922080898, -5.959266323858942451E-17 ) ) ;
#17213=CARTESIAN_POINT ( 'NONE',  ( 41.24356139695900225, 11.92996613406540085, 18.89999999999999858 ) ) ;
#17222=AXIS2_PLACEMENT_3D ( 'NONE', #13187, #11066, #18300 ) ;
#17224=DIRECTION ( 'NONE',  ( 0.000000000000000000, -1.000000000000000000, 9.876950852243829821E-14 ) ) ;
#17243=VECTOR ( 'NONE', #23326, 1000.000000000000227 ) ;
#17248=CARTESIAN_POINT ( 'NONE',  ( 59.43368109719860826, 4.124228161845699958, 3.772686752615189359E-14 ) ) ;
#17267=FACE_OUTER_BOUND ( 'NONE', #17702, .T. ) ;
#17269=CARTESIAN_POINT ( 'NONE',  ( 114.8905747189829896, 12.63019305843990026, 2.920919059678259917E-14 ) ) ;
#17270=EDGE_CURVE ( 'NONE', #11391, #4850, #16822, .T. ) ;
#17275=CARTESIAN_POINT ( 'NONE',  ( 39.74442752440959481, 5.605205456207779768, 19.59999999999999787 ) ) ;
#17285=ORIENTED_EDGE ( 'NONE', *, *, #18811, .F. ) ;
#17302=DIRECTION ( 'NONE',  ( -0.2306359803922054252, -0.9730401042858028982, 0.000000000000000000 ) ) ;
#17303=ORIENTED_EDGE ( 'NONE', *, *, #14363, .T. ) ;
#17307=DIRECTION ( 'NONE',  ( -0.9730401042858024541, 0.2306359803922080898, 5.959266323858942451E-17 ) ) ;
#17321=DIRECTION ( 'NONE',  ( -0.9730401042858022320, 0.2306359803922080343, 5.959266323858941219E-17 ) ) ;
#17325=DIRECTION ( 'NONE',  ( -0.9730401042858024541, 0.2306359803922080898, 5.959266323858942451E-17 ) ) ;
#17326=ORIENTED_EDGE ( 'NONE', *, *, #5199, .F. ) ;
#17328=AXIS2_PLACEMENT_3D ( 'NONE', #6364, #13846, #13604 ) ;
#17346=ORIENTED_EDGE ( 'NONE', *, *, #17179, .T. ) ;
#17361=AXIS2_PLACEMENT_3D ( 'NONE', #7722, #22307, #15189 ) ;
#17364=ORIENTED_EDGE ( 'NONE', *, *, #7830, .F. ) ;
#17369=ORIENTED_EDGE ( 'NONE', *, *, #18380, .F. ) ;
#17378=AXIS2_PLACEMENT_3D ( 'NONE', #22376, #9336, #5770 ) ;
#17380=PLANE ( 'NONE',  #10009 ) ;
#17404=ORIENTED_EDGE ( 'NONE', *, *, #8399, .F. ) ;
#17414=DIRECTION ( 'NONE',  ( -0.9730401042858024541, 0.2306359803922080898, 5.959266323858942451E-17 ) ) ;
#17437=DIRECTION ( 'NONE',  ( -7.440628469791170033E-16, -2.880774829024070580E-15, -1.000000000000000000 ) ) ;
#17450=CARTESIAN_POINT ( 'NONE',  ( 114.3964932440919995, -22.26358663789240211, 13.00000000000000000 ) ) ;
#17462=PLANE ( 'NONE',  #23236 ) ;
#17475=LINE ( 'NONE', #10137, #828 ) ;
#17478=ADVANCED_FACE ( 'NONE', ( #18061 ), #20640, .F. ) ;
#17484=CARTESIAN_POINT ( 'NONE',  ( 118.5310588935630136, -6.697506338400819992, 20.00000000000000000 ) ) ;
#17500=DIRECTION ( 'NONE',  ( -0.2306359803922066187, -0.9730401042858026761, 0.000000000000000000 ) ) ;
#17508=LINE ( 'NONE', #23067, #3863 ) ;
#17516=ORIENTED_EDGE ( 'NONE', *, *, #23001, .T. ) ;
#17527=CARTESIAN_POINT ( 'NONE',  ( 114.6071564266699880, -22.31351932764730250, -13.00000000000000000 ) ) ;
#17545=ORIENTED_EDGE ( 'NONE', *, *, #18854, .F. ) ;
#17547=EDGE_CURVE ( 'NONE', #15073, #2908, #1771, .T. ) ;
#17551=ORIENTED_EDGE ( 'NONE', *, *, #892, .F. ) ;
#17563=DIRECTION ( 'NONE',  ( 0.9730401042858024541, -0.2306359803922080898, -5.959266323858942451E-17 ) ) ;
#17564=VECTOR ( 'NONE', #17720, 1000.000000000000114 ) ;
#17567=CARTESIAN_POINT ( 'NONE',  ( 56.55073134229600385, -8.038773141726823113, 3.790339717502946186E-14 ) ) ;
#17580=ORIENTED_EDGE ( 'NONE', *, *, #15661, .T. ) ;
#17585=VECTOR ( 'NONE', #21158, 1000.000000000000227 ) ;
#17599=CARTESIAN_POINT ( 'NONE',  ( 36.10037903421270755, -9.768828191507939351, 3.399999999999999911 ) ) ;
#17601=CIRCLE ( 'NONE', #10412, 12.50000000000000000 ) ;
#17603=LINE ( 'NONE', #4651, #20114 ) ;
#17605=ORIENTED_EDGE ( 'NONE', *, *, #8323, .T. ) ;
#17608=DIRECTION ( 'NONE',  ( 0.9730401042858024541, -0.2306359803922080898, -5.959266323858942451E-17 ) ) ;
#17610=DIRECTION ( 'NONE',  ( -0.2306359803922077290, -0.9730401042858024541, 0.000000000000000000 ) ) ;
#17620=CARTESIAN_POINT ( 'NONE',  ( 114.3964932440919995, -22.26358663789240211, -13.00000000000000000 ) ) ;
#17627=CARTESIAN_POINT ( 'NONE',  ( 120.6036919168680015, 2.985523383783569962, 13.00000000000000000 ) ) ;
#17629=CARTESIAN_POINT ( 'NONE',  ( 55.46237324781409939, -8.294657213477510282, 13.00000000000000000 ) ) ;
#17635=EDGE_LOOP ( 'NONE', ( #9268, #12907 ) ) ;
#17638=ORIENTED_EDGE ( 'NONE', *, *, #8080, .T. ) ;
#17645=DIRECTION ( 'NONE',  ( -0.9730401042858022320, 0.2306359803922080343, 5.959266323858941219E-17 ) ) ;
#17649=VECTOR ( 'NONE', #9047, 1000.000000000000114 ) ;
#17661=DIRECTION ( 'NONE',  ( -0.2306359803922053142, -0.9730401042858028982, 0.000000000000000000 ) ) ;
#17663=CARTESIAN_POINT ( 'NONE',  ( 105.8171986446039909, -20.23006919877430221, -13.00000000000000000 ) ) ;
#17664=ORIENTED_EDGE ( 'NONE', *, *, #21250, .T. ) ;
#17667=EDGE_LOOP ( 'NONE', ( #16008, #20856, #10224, #8818 ) ) ;
#17674=EDGE_CURVE ( 'NONE', #22958, #15635, #3786, .T. ) ;
#17685=FACE_OUTER_BOUND ( 'NONE', #21198, .T. ) ;
#17686=EDGE_LOOP ( 'NONE', ( #19068, #22849, #4985, #8260 ) ) ;
#17689=CARTESIAN_POINT ( 'NONE',  ( 35.84667945578129888, -10.83917230622230043, -3.099999999999909939 ) ) ;
#17695=DIRECTION ( 'NONE',  ( -0.2306359803922053697, -0.9730401042858028982, 0.000000000000000000 ) ) ;
#17701=ORIENTED_EDGE ( 'NONE', *, *, #12008, .F. ) ;
#17702=EDGE_LOOP ( 'NONE', ( #11967, #23094, #22340, #21464 ) ) ;
#17705=ADVANCED_FACE ( 'NONE', ( #3678 ), #5933, .T. ) ;
#17715=FACE_OUTER_BOUND ( 'NONE', #5940, .T. ) ;
#17716=CARTESIAN_POINT ( 'NONE',  ( 39.74442752440959481, 5.605205456207790427, 20.00000000000000000 ) ) ;
#17720=DIRECTION ( 'NONE',  ( 0.1187863113461966047, 0.5011527021216413136, -0.8571673007021102242 ) ) ;
#17722=FACE_OUTER_BOUND ( 'NONE', #16830, .T. ) ;
#17725=EDGE_LOOP ( 'NONE', ( #21607, #8559, #19527, #23255 ) ) ;
#17728=CARTESIAN_POINT ( 'NONE',  ( 117.1241794131700118, -12.63305097454430026, 15.90000000000000036 ) ) ;
#17745=FACE_OUTER_BOUND ( 'NONE', #17725, .T. ) ;
#17749=EDGE_LOOP ( 'NONE', ( #2238, #13943 ) ) ;
#17759=CARTESIAN_POINT ( 'NONE',  ( 115.3944095602285387, -19.93085175668762332, -13.00000000000000000 ) ) ;
#17772=ORIENTED_EDGE ( 'NONE', *, *, #21301, .F. ) ;
#17773=CARTESIAN_POINT ( 'NONE',  ( 117.1933702072879981, -12.34113894325849969, 19.59999999999999787 ) ) ;
#17780=ORIENTED_EDGE ( 'NONE', *, *, #16966, .F. ) ;
#17788=CLOSED_SHELL ( 'NONE', ( #8083, #23048, #20749, #17478, #13865, #4878, #11470, #2711, #7402, #20843, #9261, #7541, #2369, #12295, #3904, #21469, #2291, #13729, #926, #5305, #12587, #18134, #16246, #7957, #4450, #20265, #4451, #10149, #22152, #10265, #14047, #4539, #20964, #9936, #21239, #20965, #15163, #16528, #20055, #22134, #7795, #22460, #3172, #64, #6454, #23315, #22415, #4333, #117, #15942, #13158, #5796, #11160, #770, #20797, #19341, #972, #11764, #7574, #14792, #16028, #11478, #1711, #976, #20559, #12278, #1470, #3027, #10394, #7162, #7287, #22751, #19596, #15510, #7361, #2987, #2640, #4346, #21448, #22395, #20656, #3197, #13609, #9059, #17705, #4541, #22494, #7611, #5565, #18555, #14146, #15231, #22791, #846, #20700, #4550, #21802, #4022, #8223, #18527, #20984, #13277, #1438, #4586, #12806, #22612, #21145, #11523, #2266, #13688, #20275 ) ) ;
#17800=EDGE_CURVE ( 'NONE', #2277, #1222, #8892, .T. ) ;
#17807=EDGE_CURVE ( 'NONE', #19697, #227, #5090, .T. ) ;
#17824=VECTOR ( 'NONE', #20777, 1000.000000000000000 ) ;
#17831=VERTEX_POINT ( 'NONE', #19231 ) ;
#17841=DIRECTION ( 'NONE',  ( 0.000000000000000000, 0.000000000000000000, -1.000000000000000000 ) ) ;
#17851=VECTOR ( 'NONE', #10970, 1000.000000000000114 ) ;
#17856=DIRECTION ( 'NONE',  ( -0.9730401042858022320, 0.2306359803922080343, 5.959266323858941219E-17 ) ) ;
#17864=CARTESIAN_POINT ( 'NONE',  ( 37.46113131852679601, -4.027891576221660053, 13.00000000000000000 ) ) ;
#17866=AXIS2_PLACEMENT_3D ( 'NONE', #9603, #23088, #14083 ) ;
#17867=DIRECTION ( 'NONE',  ( 1.749697687229200179E-14, 7.407713590345340554E-14, -1.000000000000000000 ) ) ;
#17876=CYLINDRICAL_SURFACE ( 'NONE', #15087, 0.3999999999999982458 ) ;
#17883=DIRECTION ( 'NONE',  ( -0.2306359803922076734, -0.9730401042858024541, 1.412237191019896754E-17 ) ) ;
#17885=LINE ( 'NONE', #19905, #5065 ) ;
#17892=CIRCLE ( 'NONE', #21670, 2.066999999999998394 ) ;
#17901=EDGE_CURVE ( 'NONE', #9054, #104, #10221, .T. ) ;
#17909=EDGE_CURVE ( 'NONE', #21550, #23097, #6616, .T. ) ;
#17918=ORIENTED_EDGE ( 'NONE', *, *, #4633, .F. ) ;
#17925=ORIENTED_EDGE ( 'NONE', *, *, #10875, .F. ) ;
#17945=EDGE_CURVE ( 'NONE', #19198, #2339, #19695, .T. ) ;
#17954=CIRCLE ( 'NONE', #11907, 0.4000000000000010214 ) ;
#17958=CARTESIAN_POINT ( 'NONE',  ( 44.03425675970473208, 23.70375139592372449, -13.00000000000000000 ) ) ;
#17971=EDGE_CURVE ( 'NONE', #131, #8021, #10342, .T. ) ;
#17975=VECTOR ( 'NONE', #23333, 1000.000000000000227 ) ;
#17976=AXIS2_PLACEMENT_3D ( 'NONE', #13398, #13508, #13625 ) ;
#17980=ORIENTED_EDGE ( 'NONE', *, *, #12685, .F. ) ;
#17984=CARTESIAN_POINT ( 'NONE',  ( 114.2412296582679971, -24.79605227811670076, -2.999999999999940048 ) ) ;
#17990=FACE_OUTER_BOUND ( 'NONE', #7015, .T. ) ;
#17997=EDGE_CURVE ( 'NONE', #11146, #23127, #12323, .T. ) ;
#17999=CARTESIAN_POINT ( 'NONE',  ( 36.88454136754629076, -6.460491836936111731, 13.00000000000000000 ) ) ;
#18009=FACE_OUTER_BOUND ( 'NONE', #7393, .T. ) ;
#18020=CYLINDRICAL_SURFACE ( 'NONE', #824, 2.066999999999999726 ) ;
#18027=DIRECTION ( 'NONE',  ( 0.2306359803922087282, 0.9730401042858021210, 2.478176394252581732E-15 ) ) ;
#18032=ORIENTED_EDGE ( 'NONE', *, *, #11009, .T. ) ;
#18038=CYLINDRICAL_SURFACE ( 'NONE', #11495, 2.066999999999998394 ) ;
#18042=ORIENTED_EDGE ( 'NONE', *, *, #19847, .F. ) ;
#18044=EDGE_LOOP ( 'NONE', ( #11697, #5350, #676, #5685 ) ) ;
#18056=CARTESIAN_POINT ( 'NONE',  ( 115.1338136878955964, -20.09158224951067240, -13.00000000000000000 ) ) ;
#18058=CIRCLE ( 'NONE', #21087, 2.066999999999998394 ) ;
#18059=EDGE_CURVE ( 'NONE', #2209, #23363, #1398, .T. ) ;
#18060=FACE_OUTER_BOUND ( 'NONE', #702, .T. ) ;
#18061=FACE_OUTER_BOUND ( 'NONE', #21500, .T. ) ;
#18062=LINE ( 'NONE', #19957, #11885 ) ;
#18063=VERTEX_POINT ( 'NONE', #12360 ) ;
#18075=LINE ( 'NONE', #9049, #5927 ) ;
#18077=AXIS2_PLACEMENT_3D ( 'NONE', #11169, #18507, #14808 ) ;
#18082=FACE_OUTER_BOUND ( 'NONE', #18664, .T. ) ;
#18117=CARTESIAN_POINT ( 'NONE',  ( 118.5310588935630136, -6.697506338400810222, 19.59999999999999787 ) ) ;
#18118=DIRECTION ( 'NONE',  ( 0.2306359803922080898, 0.9730401042858024541, -2.572202231434325988E-16 ) ) ;
#18128=AXIS2_PLACEMENT_3D ( 'NONE', #17269, #22587, #8238 ) ;
#18131=VECTOR ( 'NONE', #4818, 1000.000000000000227 ) ;
#18132=DIRECTION ( 'NONE',  ( -0.9730401042858024541, 0.2306359803922080898, 5.959266323858942451E-17 ) ) ;
#18133=ORIENTED_EDGE ( 'NONE', *, *, #20854, .T. ) ;
#18134=ADVANCED_FACE ( 'NONE', ( #5552 ), #18038, .F. ) ;
#18141=VECTOR ( 'NONE', #7335, 1000.000000000000114 ) ;
#18149=ORIENTED_EDGE ( 'NONE', *, *, #10219, .F. ) ;
#18150=CARTESIAN_POINT ( 'NONE',  ( 55.93909781928478253, -6.283383317918767474, 13.00000000000000000 ) ) ;
#18151=CARTESIAN_POINT ( 'NONE',  ( 37.88245768368250310, -4.127756955731490152, 13.00000000000000000 ) ) ;
#18162=VECTOR ( 'NONE', #17051, 1000.000000000000114 ) ;
#18165=PLANE ( 'NONE',  #20706 ) ;
#18173=DIRECTION ( 'NONE',  ( 0.1630842657209385649, 0.6880432561069587116, 0.7071067811865449082 ) ) ;
#18180=DIRECTION ( 'NONE',  ( 0.2306359803922080343, 0.9730401042858022320, -1.412237191019910313E-17 ) ) ;
#18184=ORIENTED_EDGE ( 'NONE', *, *, #16123, .T. ) ;
#18186=CARTESIAN_POINT ( 'NONE',  ( 45.07211867146970263, 28.08243186520990164, -13.00000000000000000 ) ) ;
#18188=CARTESIAN_POINT ( 'NONE',  ( 114.8905747189829896, 12.63019305843990026, 2.920919059678259917E-14 ) ) ;
#18189=LINE ( 'NONE', #12960, #7609 ) ;
#18196=ORIENTED_EDGE ( 'NONE', *, *, #12759, .F. ) ;
#18202=CARTESIAN_POINT ( 'NONE',  ( 39.76749112244890227, 5.702509466636359825, -15.90000000000000036 ) ) ;
#18212=VECTOR ( 'NONE', #17645, 1000.000000000000227 ) ;
#18214=CIRCLE ( 'NONE', #7980, 2.066999999999998394 ) ;
#18225=CARTESIAN_POINT ( 'NONE',  ( 96.81657767996070163, -18.09668638014640152, -13.00000000000000000 ) ) ;
#18233=CARTESIAN_POINT ( 'NONE',  ( 43.66832999130209458, 21.22121844545429781, 13.00000000000000000 ) ) ;
#18241=ORIENTED_EDGE ( 'NONE', *, *, #9731, .F. ) ;
#18262=VERTEX_POINT ( 'NONE', #4244 ) ;
#18269=CYLINDRICAL_SURFACE ( 'NONE', #18077, 2.066999999999999726 ) ;
#18270=CARTESIAN_POINT ( 'NONE',  ( 38.35918225515318625, -2.116483060172758446, -13.00000000000000000 ) ) ;
#18287=DIRECTION ( 'NONE',  ( -0.9730401042858024541, 0.2306359803922080898, 5.959266323862662423E-17 ) ) ;
#18294=AXIS2_PLACEMENT_3D ( 'NONE', #14265, #20075, #21503 ) ;
#18300=DIRECTION ( 'NONE',  ( -0.9730401042858022320, 0.2306359803922080343, 5.252801108490690349E-31 ) ) ;
#18309=VERTEX_POINT ( 'NONE', #22401 ) ;
#18315=AXIS2_PLACEMENT_3D ( 'NONE', #23307, #3483, #12858 ) ;
#18318=VECTOR ( 'NONE', #21942, 1000.000000000000227 ) ;
#18326=VECTOR ( 'NONE', #15849, 1000.000000000000227 ) ;
#18329=DIRECTION ( 'NONE',  ( -0.9730401042858024541, 0.2306359803922080898, 5.959266323858942451E-17 ) ) ;
#18331=LINE ( 'NONE', #3950, #4058 ) ;
#18333=ORIENTED_EDGE ( 'NONE', *, *, #13795, .F. ) ;
#18334=CONICAL_SURFACE ( 'NONE', #11542, 2.283499999999998753, 0.7853981633974433940 ) ;
#18336=VECTOR ( 'NONE', #15776, 1000.000000000000227 ) ;
#18342=CARTESIAN_POINT ( 'NONE',  ( 45.41807264205800010, 29.54199202163849947, -9.133960000000000079 ) ) ;
#18344=AXIS2_PLACEMENT_3D ( 'NONE', #19263, #8334, #11486 ) ;
#18346=DIRECTION ( 'NONE',  ( 2.199957270157979832E-13, -9.825194207785550278E-30, -1.000000000000000000 ) ) ;
#18348=VECTOR ( 'NONE', #10991, 1000.000000000000227 ) ;
#18352=EDGE_CURVE ( 'NONE', #16389, #14157, #511, .T. ) ;
#18356=CARTESIAN_POINT ( 'NONE',  ( 37.46113131852679601, -4.027891576221570347, 20.00000000000000000 ) ) ;
#18358=CIRCLE ( 'NONE', #8120, 0.4000000000000010214 ) ;
#18360=AXIS2_PLACEMENT_3D ( 'NONE', #11660, #20658, #6524 ) ;
#18370=CARTESIAN_POINT ( 'NONE',  ( 39.83668191656649782, 5.994421497922140851, 18.89999999999999858 ) ) ;
#18375=ORIENTED_EDGE ( 'NONE', *, *, #11122, .F. ) ;
#18377=FACE_BOUND ( 'NONE', #700, .T. ) ;
#18380=EDGE_CURVE ( 'NONE', #2609, #15201, #22752, .T. ) ;
#18400=DIRECTION ( 'NONE',  ( 0.000000000000000000, 0.000000000000000000, 1.000000000000000000 ) ) ;
#18422=CARTESIAN_POINT ( 'NONE',  ( 113.2033677465029911, -29.17473274740279976, -13.00000000000000000 ) ) ;
#18424=DIRECTION ( 'NONE',  ( -0.9730401042858022320, 0.2306359803922080343, 5.959266323858941219E-17 ) ) ;
#18434=CARTESIAN_POINT ( 'NONE',  ( 36.10037903421270755, -9.768828191507928693, 2.700000000000049916 ) ) ;
#18446=ORIENTED_EDGE ( 'NONE', *, *, #15808, .F. ) ;
#18450=CARTESIAN_POINT ( 'NONE',  ( 106.2939232160746883, -18.21879530321555052, -13.00000000000000000 ) ) ;
#18452=ORIENTED_EDGE ( 'NONE', *, *, #5222, .T. ) ;
#18474=CARTESIAN_POINT ( 'NONE',  ( 120.6036919168680015, 2.985523383783569962, 13.00000000000000000 ) ) ;
#18499=ORIENTED_EDGE ( 'NONE', *, *, #4901, .F. ) ;
#18507=DIRECTION ( 'NONE',  ( 0.2306359803922080898, 0.9730401042858024541, -2.572202231434325988E-16 ) ) ;
#18512=EDGE_CURVE ( 'NONE', #8379, #7119, #17601, .T. ) ;
#18527=ADVANCED_FACE ( 'NONE', ( #6630 ), #1136, .F. ) ;
#18542=VERTEX_POINT ( 'NONE', #13862 ) ;
#18544=CARTESIAN_POINT ( 'NONE',  ( 36.88454136754629786, -6.460491836936129495, -2.999999999999930278 ) ) ;
#18555=ADVANCED_FACE ( 'NONE', ( #6745 ), #21336, .T. ) ;
#18557=EDGE_LOOP ( 'NONE', ( #12362, #2617, #2934, #5929 ) ) ;
#18562=LINE ( 'NONE', #20794, #20874 ) ;
#18570=FACE_OUTER_BOUND ( 'NONE', #19120, .T. ) ;
#18574=FACE_OUTER_BOUND ( 'NONE', #12236, .T. ) ;
#18584=CARTESIAN_POINT ( 'NONE',  ( 52.45828777336790694, 19.13776831658130106, 13.00000000000000000 ) ) ;
#18597=CIRCLE ( 'NONE', #15548, 2.066999999999999726 ) ;
#18616=ORIENTED_EDGE ( 'NONE', *, *, #9954, .T. ) ;
#18620=AXIS2_PLACEMENT_3D ( 'NONE', #5119, #3330, #7568 ) ;
#18634=EDGE_CURVE ( 'NONE', #5198, #13888, #5641, .T. ) ;
#18642=CARTESIAN_POINT ( 'NONE',  ( 43.45766680872420551, 21.27115113520920175, 13.00000000000000000 ) ) ;
#18648=DIRECTION ( 'NONE',  ( 0.2306359803922077290, 0.9730401042858024541, -1.412237191019971018E-17 ) ) ;
#18659=LINE ( 'NONE', #13306, #21600 ) ;
#18664=EDGE_LOOP ( 'NONE', ( #5531, #19573, #7800, #2452 ) ) ;
#18678=ORIENTED_EDGE ( 'NONE', *, *, #22160, .F. ) ;
#18686=EDGE_LOOP ( 'NONE', ( #429, #11368, #5903, #9098 ) ) ;
#18698=DIRECTION ( 'NONE',  ( 1.734723475976802677E-14, 9.540979117872415038E-14, -1.000000000000000000 ) ) ;
#18723=DIRECTION ( 'NONE',  ( 0.2306359803922080343, 0.9730401042858022320, -2.974717104243940401E-15 ) ) ;
#18738=CARTESIAN_POINT ( 'NONE',  ( 59.43368109719860826, 4.124228161845699958, 3.772686752615189359E-14 ) ) ;
#18744=VECTOR ( 'NONE', #3537, 1000.000000000000227 ) ;
#18768=ORIENTED_EDGE ( 'NONE', *, *, #7941, .F. ) ;
#18769=VERTEX_POINT ( 'NONE', #7205 ) ;
#18774=DIRECTION ( 'NONE',  ( -0.9730401042858024541, 0.2306359803922080898, 5.959266323858952312E-17 ) ) ;
#18786=ORIENTED_EDGE ( 'NONE', *, *, #21593, .T. ) ;
#18791=EDGE_LOOP ( 'NONE', ( #19576, #4509 ) ) ;
#18798=EDGE_CURVE ( 'NONE', #7119, #8379, #11886, .T. ) ;
#18809=DIRECTION ( 'NONE',  ( 0.2306359803922080343, 0.9730401042858022320, 5.907067092757291018E-15 ) ) ;
#18811=EDGE_CURVE ( 'NONE', #16103, #19758, #21712, .T. ) ;
#18825=CIRCLE ( 'NONE', #3631, 2.500000000000000000 ) ;
#18834=DIRECTION ( 'NONE',  ( -2.920245690604589998E-14, -1.234618914536939803E-13, 1.000000000000000000 ) ) ;
#18844=ORIENTED_EDGE ( 'NONE', *, *, #21307, .T. ) ;
#18846=ORIENTED_EDGE ( 'NONE', *, *, #1038, .F. ) ;
#18854=EDGE_CURVE ( 'NONE', #15831, #12377, #13366, .T. ) ;
#18855=CARTESIAN_POINT ( 'NONE',  ( 102.3363885986873356, 5.191082435725835609, 13.00000000000000000 ) ) ;
#18856=ORIENTED_EDGE ( 'NONE', *, *, #20028, .F. ) ;
#18858=EDGE_CURVE ( 'NONE', #23125, #15635, #20368, .T. ) ;
#18862=CARTESIAN_POINT ( 'NONE',  ( 121.3909450504253584, 5.368190954742520837, 13.00000000000000000 ) ) ;
#18869=ORIENTED_EDGE ( 'NONE', *, *, #1057, .F. ) ;
#18879=AXIS2_PLACEMENT_3D ( 'NONE', #18584, #2431, #16786 ) ;
#18884=ORIENTED_EDGE ( 'NONE', *, *, #18512, .F. ) ;
#18886=FACE_OUTER_BOUND ( 'NONE', #7268, .T. ) ;
#18889=CARTESIAN_POINT ( 'NONE',  ( 96.81657767996070163, -18.09668638014640152, 13.00000000000000000 ) ) ;
#18891=AXIS2_PLACEMENT_3D ( 'NONE', #16385, #7487, #11065 ) ;
#18899=ORIENTED_EDGE ( 'NONE', *, *, #22689, .T. ) ;
#18912=DIRECTION ( 'NONE',  ( -0.9730401042858023430, 0.2306359803922080620, 5.959266323858944916E-17 ) ) ;
#18915=DIRECTION ( 'NONE',  ( -0.9730401042858022320, 0.2306359803922080343, 5.959266323858941219E-17 ) ) ;
#18920=ORIENTED_EDGE ( 'NONE', *, *, #11599, .F. ) ;
#18942=ORIENTED_EDGE ( 'NONE', *, *, #17997, .T. ) ;
#18961=EDGE_CURVE ( 'NONE', #16110, #131, #10286, .T. ) ;
#18970=DIRECTION ( 'NONE',  ( -0.9730401042858022320, 0.2306359803922080343, 5.959266323858941219E-17 ) ) ;
#19004=CARTESIAN_POINT ( 'NONE',  ( 39.30621916166446539, 3.756429258064753807, 3.834721291928176309E-14 ) ) ;
#19011=VERTEX_POINT ( 'NONE', #8374 ) ;
#19016=CARTESIAN_POINT ( 'NONE',  ( 59.43368109719860826, 4.124228161845699958, 3.772686752615189359E-14 ) ) ;
#19028=DIRECTION ( 'NONE',  ( 0.9730401042858024541, -0.2306359803922080898, -5.959266323858232476E-17 ) ) ;
#19035=CYLINDRICAL_SURFACE ( 'NONE', #4643, 0.4000000000000010214 ) ;
#19047=DIRECTION ( 'NONE',  ( 0.2306359803922094498, 0.9730401042858018990, 0.000000000000000000 ) ) ;
#19049=CARTESIAN_POINT ( 'NONE',  ( 118.4388045014059969, -7.086722380115170417, -18.89999999999999858 ) ) ;
#19051=LINE ( 'NONE', #4679, #14301 ) ;
#19059=DIRECTION ( 'NONE',  ( -0.9730401042858022320, 0.2306359803922080343, 5.959266323858941219E-17 ) ) ;
#19068=ORIENTED_EDGE ( 'NONE', *, *, #738, .T. ) ;
#19079=DIRECTION ( 'NONE',  ( -0.9730401042858022320, 0.2306359803922080343, 5.959266323858941219E-17 ) ) ;
#19091=FACE_OUTER_BOUND ( 'NONE', #10504, .T. ) ;
#19096=ORIENTED_EDGE ( 'NONE', *, *, #22385, .T. ) ;
#19111=VERTEX_POINT ( 'NONE', #6464 ) ;
#19112=CARTESIAN_POINT ( 'NONE',  ( 105.3404740731333078, -22.24134309433305390, -13.00000000000000000 ) ) ;
#19120=EDGE_LOOP ( 'NONE', ( #18241, #504, #19494, #5072 ) ) ;
#19121=SHAPE_DEFINITION_REPRESENTATION ( #19712, #20540 ) ;
#19122=EDGE_CURVE ( 'NONE', #4506, #14346, #13712, .T. ) ;
#19145=CARTESIAN_POINT ( 'NONE',  ( 50.62112045032230156, 16.80665986293769976, 3.576075166576559901E-14 ) ) ;
#19156=EDGE_LOOP ( 'NONE', ( #17303, #11591, #12677, #18184 ) ) ;
#19161=VERTEX_POINT ( 'NONE', #10877 ) ;
#19162=EDGE_CURVE ( 'NONE', #227, #18542, #23, .T. ) ;
#19164=DIRECTION ( 'NONE',  ( -2.573454422195745135E-14, 0.000000000000000000, -1.000000000000000000 ) ) ;
#19180=CARTESIAN_POINT ( 'NONE',  ( 37.46113131852679601, -4.027891576221570347, 20.00000000000000000 ) ) ;
#19185=DIRECTION ( 'NONE',  ( -0.2306359803922077290, -0.9730401042858024541, 0.000000000000000000 ) ) ;
#19191=LINE ( 'NONE', #6611, #1781 ) ;
#19198=VERTEX_POINT ( 'NONE', #1699 ) ;
#19231=CARTESIAN_POINT ( 'NONE',  ( 44.03425675970473208, 23.70375139592372449, 13.00000000000000000 ) ) ;
#19234=VERTEX_POINT ( 'NONE', #8850 ) ;
#19252=DIRECTION ( 'NONE',  ( -0.2306359803922094498, -0.9730401042858020100, 1.412237191019847142E-17 ) ) ;
#19263=CARTESIAN_POINT ( 'NONE',  ( 117.1241794131700118, -12.63305097454420078, -15.90000000000000036 ) ) ;
#19270=VERTEX_POINT ( 'NONE', #148 ) ;
#19279=AXIS2_PLACEMENT_3D ( 'NONE', #22777, #6289, #15420 ) ;
#19285=EDGE_CURVE ( 'NONE', #4850, #13082, #20104, .T. ) ;
#19287=DIRECTION ( 'NONE',  ( 0.5249589903860194529, -0.8511275218278935295, 5.444325428271645316E-17 ) ) ;
#19289=DIRECTION ( 'NONE',  ( 0.9730401042858024541, -0.2306359803922080898, -5.959266323859062013E-17 ) ) ;
#19294=EDGE_LOOP ( 'NONE', ( #6768, #8108, #8406, #8812 ) ) ;
#19299=DIRECTION ( 'NONE',  ( 1.000000000000000000, 7.664170260637140280E-16, 0.000000000000000000 ) ) ;
#19317=VECTOR ( 'NONE', #20483, 1000.000000000000000 ) ;
#19318=CARTESIAN_POINT ( 'NONE',  ( 45.98502771169970060, -8.172548290408343519, 13.00000000000000000 ) ) ;
#19320=DIRECTION ( 'NONE',  ( -0.9730401042858024541, 0.2306359803922080898, 5.959266323863162857E-17 ) ) ;
#19341=ADVANCED_FACE ( 'NONE', ( #18574 ), #13110, .F. ) ;
#19348=ORIENTED_EDGE ( 'NONE', *, *, #23080, .T. ) ;
#19353=ORIENTED_EDGE ( 'NONE', *, *, #13173, .F. ) ;
#19368=FACE_OUTER_BOUND ( 'NONE', #17096, .T. ) ;
#19370=EDGE_LOOP ( 'NONE', ( #22441, #19987, #11808, #16615 ) ) ;
#19387=CARTESIAN_POINT ( 'NONE',  ( 50.76434296088209663, 17.41090750189739822, 3.560102062092729998E-14 ) ) ;
#19394=DIRECTION ( 'NONE',  ( -1.000000000000000000, 0.000000000000000000, -3.525869238601989755E-16 ) ) ;
#19402=CYLINDRICAL_SURFACE ( 'NONE', #22227, 2.066999999999999726 ) ;
#19415=CARTESIAN_POINT ( 'NONE',  ( 41.24356139695900225, 11.92996613406550033, -18.89999999999999858 ) ) ;
#19428=FACE_OUTER_BOUND ( 'NONE', #19156, .T. ) ;
#19434=VECTOR ( 'NONE', #15702, 1000.000000000000114 ) ;
#19439=AXIS2_PLACEMENT_3D ( 'NONE', #11873, #15054, #4724 ) ;
#19445=EDGE_CURVE ( 'NONE', #12377, #2029, #17954, .T. ) ;
#19464=DIRECTION ( 'NONE',  ( 0.9730401042858024541, -0.2306359803922080898, -5.959266323858942451E-17 ) ) ;
#19465=DIRECTION ( 'NONE',  ( -0.2306359803922076457, -0.9730401042858025651, 0.000000000000000000 ) ) ;
#19476=ORIENTED_EDGE ( 'NONE', *, *, #14641, .F. ) ;
#19492=DIRECTION ( 'NONE',  ( -0.9730401042858022320, 0.2306359803922080343, 5.959266323858941219E-17 ) ) ;
#19493=CARTESIAN_POINT ( 'NONE',  ( 113.4570673249340018, -28.10438863268850085, 2.700000000000049916 ) ) ;
#19494=ORIENTED_EDGE ( 'NONE', *, *, #10914, .T. ) ;
#19495=CARTESIAN_POINT ( 'NONE',  ( 117.1011158151309957, -12.73035498497280038, 19.59999999999999787 ) ) ;
#19510=DIRECTION ( 'NONE',  ( 0.8511275218278948618, 0.5249589903860170104, -5.212440122911309516E-17 ) ) ;
#19514=ORIENTED_EDGE ( 'NONE', *, *, #8270, .T. ) ;
#19518=DIRECTION ( 'NONE',  ( -0.9730401042858022320, 0.2306359803922080343, 5.959266323858941219E-17 ) ) ;
#19519=EDGE_CURVE ( 'NONE', #18262, #9929, #15679, .T. ) ;
#19521=CARTESIAN_POINT ( 'NONE',  ( 52.45828777336780036, 19.13776831658130106, -13.00000000000000000 ) ) ;
#19527=ORIENTED_EDGE ( 'NONE', *, *, #15483, .F. ) ;
#19532=ORIENTED_EDGE ( 'NONE', *, *, #7941, .T. ) ;
#19545=ORIENTED_EDGE ( 'NONE', *, *, #13891, .F. ) ;
#19547=EDGE_CURVE ( 'NONE', #3952, #990, #10382, .T. ) ;
#19556=ORIENTED_EDGE ( 'NONE', *, *, #8180, .F. ) ;
#19560=VERTEX_POINT ( 'NONE', #2767 ) ;
#19573=ORIENTED_EDGE ( 'NONE', *, *, #8903, .F. ) ;
#19576=ORIENTED_EDGE ( 'NONE', *, *, #18512, .T. ) ;
#19577=DIRECTION ( 'NONE',  ( 1.749697687228930073E-14, 7.407713590344219741E-14, -1.000000000000000000 ) ) ;
#19578=DIRECTION ( 'NONE',  ( -0.9730401042858024541, 0.2306359803922080898, 5.959266323858942451E-17 ) ) ;
#19581=DIRECTION ( 'NONE',  ( -0.2306359803922083396, -0.9730401042858023430, -4.336808689942018998E-14 ) ) ;
#19587=ORIENTED_EDGE ( 'NONE', *, *, #15091, .F. ) ;
#19593=VECTOR ( 'NONE', #303, 1000.000000000000114 ) ;
#19594=CIRCLE ( 'NONE', #7834, 2.066999999999997506 ) ;
#19595=( NAMED_UNIT ( * ) PLANE_ANGLE_UNIT ( ) SI_UNIT ( $, .RADIAN. ) );
#19596=ADVANCED_FACE ( 'NONE', ( #6437 ), #13814, .T. ) ;
#19603=CARTESIAN_POINT ( 'NONE',  ( 53.15246078658950069, 27.48624099592299785, 2.283500000000032948 ) ) ;
#19608=ORIENTED_EDGE ( 'NONE', *, *, #13329, .F. ) ;
#19611=EDGE_CURVE ( 'NONE', #21109, #10345, #6200, .T. ) ;
#19613=ORIENTED_EDGE ( 'NONE', *, *, #14009, .F. ) ;
#19615=CARTESIAN_POINT ( 'NONE',  ( 119.9163041628193440, 1.024182177979865882, 13.00000000000000000 ) ) ;
#19621=CARTESIAN_POINT ( 'NONE',  ( 36.10037903421270755, -9.768828191507889613, -3.399999999999939959 ) ) ;
#19624=CONICAL_SURFACE ( 'NONE', #18891, 2.283499999999998753, 0.7853981633974433940 ) ;
#19631=DIRECTION ( 'NONE',  ( 0.9730401042858024541, -0.2306359803922080898, -5.959266323858952312E-17 ) ) ;
#19633=LINE ( 'NONE', #12303, #21975 ) ;
#19641=EDGE_LOOP ( 'NONE', ( #2904, #4739, #12920, #21042 ) ) ;
#19643=DIRECTION ( 'NONE',  ( 0.000000000000000000, 0.000000000000000000, 1.000000000000000000 ) ) ;
#19652=DIRECTION ( 'NONE',  ( -1.734723475976802677E-14, -1.084202172485501657E-13, 1.000000000000000000 ) ) ;
#19656=DIRECTION ( 'NONE',  ( -0.2306359803922053142, -0.9730401042858028982, 0.000000000000000000 ) ) ;
#19661=DIRECTION ( 'NONE',  ( -0.2306359803921919083, -0.9730401042858062288, -4.336808689942036669E-14 ) ) ;
#19672=ORIENTED_EDGE ( 'NONE', *, *, #7453, .F. ) ;
#19678=CARTESIAN_POINT ( 'NONE',  ( 118.4388045014059969, -7.086722380115159758, -19.59999999999999787 ) ) ;
#19681=EDGE_CURVE ( 'NONE', #11043, #2245, #11159, .T. ) ;
#19685=FACE_OUTER_BOUND ( 'NONE', #13565, .T. ) ;
#19688=ORIENTED_EDGE ( 'NONE', *, *, #23344, .T. ) ;
#19691=CARTESIAN_POINT ( 'NONE',  ( 61.45890873801150178, 17.00438549795330090, -13.00000000000000000 ) ) ;
#19695=LINE ( 'NONE', #8554, #911 ) ;
#19697=VERTEX_POINT ( 'NONE', #9617 ) ;
#19701=ORIENTED_EDGE ( 'NONE', *, *, #22912, .T. ) ;
#19706=EDGE_CURVE ( 'NONE', #2719, #18769, #12256, .T. ) ;
#19712=PRODUCT_DEFINITION_SHAPE ( 'NONE', 'NONE',  #1978 ) ;
#19713=ORIENTED_EDGE ( 'NONE', *, *, #9417, .T. ) ;
#19723=FACE_OUTER_BOUND ( 'NONE', #7557, .T. ) ;
#19726=FACE_OUTER_BOUND ( 'NONE', #18557, .T. ) ;
#19730=ORIENTED_EDGE ( 'NONE', *, *, #3818, .F. ) ;
#19733=DIRECTION ( 'NONE',  ( -0.2306359803922083396, -0.9730401042858023430, -1.333568672157170959E-13 ) ) ;
#19736=EDGE_CURVE ( 'NONE', #3226, #6720, #20291, .T. ) ;
#19737=DIRECTION ( 'NONE',  ( 0.000000000000000000, 0.000000000000000000, 1.000000000000000000 ) ) ;
#19740=CARTESIAN_POINT ( 'NONE',  ( 121.1303491780936099, 5.207460461920199180, 13.00000000000000000 ) ) ;
#19744=CARTESIAN_POINT ( 'NONE',  ( 45.07211867146960316, 28.08243186520980217, 10.02499999999999858 ) ) ;
#19746=VECTOR ( 'NONE', #7277, 1000.000000000000227 ) ;
#19747=CARTESIAN_POINT ( 'NONE',  ( 52.05497947389309843, 22.85602965967900246, -2.066999999999965532 ) ) ;
#19758=VERTEX_POINT ( 'NONE', #19615 ) ;
#19761=ORIENTED_EDGE ( 'NONE', *, *, #7830, .T. ) ;
#19765=DIRECTION ( 'NONE',  ( 0.9730401042858024541, -0.2306359803922080898, -5.959266323858942451E-17 ) ) ;
#19782=DIRECTION ( 'NONE',  ( 0.1982893547227609354, 0.8365715274350927766, -0.5107146084542198983 ) ) ;
#19801=AXIS2_PLACEMENT_3D ( 'NONE', #9180, #16525, #21872 ) ;
#19809=LINE ( 'NONE', #7350, #5166 ) ;
#19811=CARTESIAN_POINT ( 'NONE',  ( 36.79228697538940196, -6.849707878650479920, -3.400000000000049649 ) ) ;
#19817=DIRECTION ( 'NONE',  ( -0.9730401042858022320, 0.2306359803922080343, 5.959266323858941219E-17 ) ) ;
#19833=CARTESIAN_POINT ( 'NONE',  ( 120.3930287342899987, 3.035456073538439714, -13.00000000000000000 ) ) ;
#19847=EDGE_CURVE ( 'NONE', #21038, #7183, #12975, .T. ) ;
#19853=ORIENTED_EDGE ( 'NONE', *, *, #14630, .F. ) ;
#19854=CARTESIAN_POINT ( 'NONE',  ( 61.45890873801150178, 17.00438549795330090, -13.00000000000000000 ) ) ;
#19866=VECTOR ( 'NONE', #17182, 1000.000000000000227 ) ;
#19883=AXIS2_PLACEMENT_3D ( 'NONE', #6048, #13302, #4278 ) ;
#19889=FACE_OUTER_BOUND ( 'NONE', #8611, .T. ) ;
#19897=CARTESIAN_POINT ( 'NONE',  ( 52.05497947389309843, 22.85602965967900246, 3.416161896595049310E-14 ) ) ;
#19905=CARTESIAN_POINT ( 'NONE',  ( 122.4288069621910040, 9.746871424029270869, 10.02499999999999858 ) ) ;
#19908=ORIENTED_EDGE ( 'NONE', *, *, #20592, .T. ) ;
#19917=ORIENTED_EDGE ( 'NONE', *, *, #21765, .F. ) ;
#19933=LINE ( 'NONE', #5319, #4691 ) ;
#19945=DIRECTION ( 'NONE',  ( 3.525869238601989755E-16, 1.745928279345489864E-15, -1.000000000000000000 ) ) ;
#19951=ORIENTED_EDGE ( 'NONE', *, *, #5888, .T. ) ;
#19952=LINE ( 'NONE', #5230, #9007 ) ;
#19953=VERTEX_POINT ( 'NONE', #6501 ) ;
#19957=CARTESIAN_POINT ( 'NONE',  ( 117.1933702072879981, -12.34113894325840022, -19.59999999999999787 ) ) ;
#19973=DIRECTION ( 'NONE',  ( -0.9730401042858022320, 0.2306359803922080343, 5.959266323858941219E-17 ) ) ;
#19977=EDGE_LOOP ( 'NONE', ( #1671, #20230, #6397, #16559 ) ) ;
#19985=CIRCLE ( 'NONE', #9769, 2.499999999999999112 ) ;
#19987=ORIENTED_EDGE ( 'NONE', *, *, #2811, .F. ) ;
#19988=DIRECTION ( 'NONE',  ( 0.2306359803922085339, 0.9730401042858022320, 0.000000000000000000 ) ) ;
#19995=ORIENTED_EDGE ( 'NONE', *, *, #9729, .F. ) ;
#19997=CIRCLE ( 'NONE', #2557, 0.4000000000000001887 ) ;
#20000=EDGE_CURVE ( 'NONE', #4506, #14758, #23100, .T. ) ;
#20023=CARTESIAN_POINT ( 'NONE',  ( 120.6036919168680015, 2.985523383783529994, -13.00000000000000000 ) ) ;
#20024=ORIENTED_EDGE ( 'NONE', *, *, #5172, .T. ) ;
#20025=CARTESIAN_POINT ( 'NONE',  ( 99.36449593087139931, -18.18675627898399583, 3.528131999253151732E-14 ) ) ;
#20028=EDGE_CURVE ( 'NONE', #1580, #12377, #1268, .T. ) ;
#20050=CARTESIAN_POINT ( 'NONE',  ( 122.7747609327790030, 11.20643158045800014, 9.133960000000000079 ) ) ;
#20054=DIRECTION ( 'NONE',  ( -0.9730401042858024541, 0.2306359803922080898, 5.959266323858942451E-17 ) ) ;
#20055=ADVANCED_FACE ( 'NONE', ( #23342 ), #18020, .F. ) ;
#20061=DIRECTION ( 'NONE',  ( -0.9730401042858023430, 0.2306359803922080620, 5.959266323858944916E-17 ) ) ;
#20066=ORIENTED_EDGE ( 'NONE', *, *, #498, .F. ) ;
#20074=ORIENTED_EDGE ( 'NONE', *, *, #21803, .F. ) ;
#20075=DIRECTION ( 'NONE',  ( -0.9730401042858024541, 0.2306359803922080898, 5.959266323858942451E-17 ) ) ;
#20098=EDGE_CURVE ( 'NONE', #20342, #13027, #21455, .T. ) ;
#20102=ORIENTED_EDGE ( 'NONE', *, *, #18634, .F. ) ;
#20104=LINE ( 'NONE', #256, #7707 ) ;
#20107=ORIENTED_EDGE ( 'NONE', *, *, #9478, .T. ) ;
#20109=CYLINDRICAL_SURFACE ( 'NONE', #882, 2.999999999999999556 ) ;
#20114=VECTOR ( 'NONE', #19492, 1000.000000000000227 ) ;
#20117=DIRECTION ( 'NONE',  ( 5.500811659918190397E-13, 0.000000000000000000, -1.000000000000000000 ) ) ;
#20131=CIRCLE ( 'NONE', #12926, 2.066999999999998394 ) ;
#20142=VERTEX_POINT ( 'NONE', #13026 ) ;
#20144=DIRECTION ( 'NONE',  ( 0.000000000000000000, 2.583840697242864839E-16, -1.000000000000000000 ) ) ;
#20151=ORIENTED_EDGE ( 'NONE', *, *, #17807, .F. ) ;
#20153=ORIENTED_EDGE ( 'NONE', *, *, #626, .F. ) ;
#20155=DIRECTION ( 'NONE',  ( -0.1982893547227720377, -0.8365715274351381847, -0.5107146084541409614 ) ) ;
#20157=DIRECTION ( 'NONE',  ( 1.460302919654610928E-28, 2.469237519705104702E-14, 1.000000000000000000 ) ) ;
#20186=CARTESIAN_POINT ( 'NONE',  ( 117.1933702072879981, -12.34113894325840022, 18.89999999999999858 ) ) ;
#20199=AXIS2_PLACEMENT_3D ( 'NONE', #8462, #11800, #1430 ) ;
#20207=LINE ( 'NONE', #123, #17649 ) ;
#20210=VECTOR ( 'NONE', #1455, 1000.000000000000227 ) ;
#20219=AXIS2_PLACEMENT_3D ( 'NONE', #17620, #11946, #8347 ) ;
#20220=ORIENTED_EDGE ( 'NONE', *, *, #15706, .F. ) ;
#20223=PLANE ( 'NONE',  #7853 ) ;
#20226=ORIENTED_EDGE ( 'NONE', *, *, #5076, .T. ) ;
#20227=VECTOR ( 'NONE', #6672, 1000.000000000000227 ) ;
#20230=ORIENTED_EDGE ( 'NONE', *, *, #19162, .T. ) ;
#20232=DIRECTION ( 'NONE',  ( 0.2306359803922080343, 0.9730401042858022320, -5.076717492620541185E-14 ) ) ;
#20265=ADVANCED_FACE ( 'NONE', ( #3637 ), #8838, .F. ) ;
#20275=ADVANCED_FACE ( 'NONE', ( #5887 ), #4104, .T. ) ;
#20284=FACE_OUTER_BOUND ( 'NONE', #14715, .T. ) ;
#20291=LINE ( 'NONE', #14264, #5768 ) ;
#20298=CIRCLE ( 'NONE', #21057, 2.999999999999999556 ) ;
#20306=ORIENTED_EDGE ( 'NONE', *, *, #22952, .F. ) ;
#20308=ORIENTED_EDGE ( 'NONE', *, *, #10858, .T. ) ;
#20309=DIRECTION ( 'NONE',  ( -0.9730401042858022320, 0.2306359803922080343, 5.959266323858941219E-17 ) ) ;
#20325=ORIENTED_EDGE ( 'NONE', *, *, #5431, .F. ) ;
#20337=DIRECTION ( 'NONE',  ( -0.9730401042858023430, 0.2306359803922080620, 5.959266323858944916E-17 ) ) ;
#20342=VERTEX_POINT ( 'NONE', #9709 ) ;
#20347=DIRECTION ( 'NONE',  ( -0.2306359803922080620, -0.9730401042858023430, 4.455014470410797513E-15 ) ) ;
#20355=CONICAL_SURFACE ( 'NONE', #10139, 2.283500000000000529, 0.7853981633974469467 ) ;
#20357=AXIS2_PLACEMENT_3D ( 'NONE', #11826, #19631, #3356 ) ;
#20368=LINE ( 'NONE', #4348, #839 ) ;
#20376=DIRECTION ( 'NONE',  ( -0.2306359803922080343, -0.9730401042858022320, -1.780177465867830349E-15 ) ) ;
#20377=VECTOR ( 'NONE', #2367, 1000.000000000000227 ) ;
#20382=ORIENTED_EDGE ( 'NONE', *, *, #19445, .T. ) ;
#20383=VECTOR ( 'NONE', #6912, 1000.000000000000000 ) ;
#20387=CIRCLE ( 'NONE', #21513, 2.066999999999997506 ) ;
#20396=EDGE_LOOP ( 'NONE', ( #20793, #4924, #4698, #19587 ) ) ;
#20425=DIRECTION ( 'NONE',  ( 0.2306359803922080898, 0.9730401042858024541, -2.572202231434325988E-16 ) ) ;
#20426=ORIENTED_EDGE ( 'NONE', *, *, #19445, .F. ) ;
#20439=PLANE ( 'NONE',  #12394 ) ;
#20440=LINE ( 'NONE', #9050, #19746 ) ;
#20444=EDGE_CURVE ( 'NONE', #5198, #9054, #537, .T. ) ;
#20445=ORIENTED_EDGE ( 'NONE', *, *, #2743, .T. ) ;
#20447=CIRCLE ( 'NONE', #2289, 2.066999999999999726 ) ;
#20449=ORIENTED_EDGE ( 'NONE', *, *, #16305, .T. ) ;
#20451=LINE ( 'NONE', #2409, #1603 ) ;
#20453=DIRECTION ( 'NONE',  ( -0.2306359803921919083, -0.9730401042858062288, -1.333568672157176260E-13 ) ) ;
#20482=CARTESIAN_POINT ( 'NONE',  ( 118.4388045014059969, -7.086722380115159758, -19.59999999999999787 ) ) ;
#20483=DIRECTION ( 'NONE',  ( -5.401314170743249993E-15, -2.304622183485879988E-14, 1.000000000000000000 ) ) ;
#20497=DIRECTION ( 'NONE',  ( -0.9730401042858024541, 0.2306359803922080898, 5.959266323858472832E-17 ) ) ;
#20503=DIRECTION ( 'NONE',  ( 0.2306359803922080343, 0.9730401042858022320, 3.574477303645861237E-15 ) ) ;
#20528=CIRCLE ( 'NONE', #13721, 2.066999999999999726 ) ;
#20529=ORIENTED_EDGE ( 'NONE', *, *, #16218, .F. ) ;
#20530=EDGE_CURVE ( 'NONE', #13027, #15043, #1347, .T. ) ;
#20537=EDGE_LOOP ( 'NONE', ( #7512, #13835, #3282, #16852 ) ) ;
#20540=SHAPE_REPRESENTATION ( '1602p_c_41', ( #12739 ), #21598 ) ;
#20548=ORIENTED_EDGE ( 'NONE', *, *, #595, .F. ) ;
#20559=ADVANCED_FACE ( 'NONE', ( #4806 ), #3020, .T. ) ;
#20572=DIRECTION ( 'NONE',  ( -0.9730401042858022320, 0.2306359803922080343, 5.959266323858941219E-17 ) ) ;
#20573=VERTEX_POINT ( 'NONE', #19415 ) ;
#20575=CARTESIAN_POINT ( 'NONE',  ( 117.6809342291340101, -10.28413402209830174, -2.440468108021579940E-14 ) ) ;
#20585=EDGE_CURVE ( 'NONE', #2245, #5079, #8855, .T. ) ;
#20590=DIRECTION ( 'NONE',  ( 0.2306359803922076457, 0.9730401042858025651, 0.000000000000000000 ) ) ;
#20592=EDGE_CURVE ( 'NONE', #14649, #13995, #16788, .T. ) ;
#20594=CARTESIAN_POINT ( 'NONE',  ( 52.45828777336790694, 19.13776831658130106, 13.00000000000000000 ) ) ;
#20611=AXIS2_PLACEMENT_3D ( 'NONE', #2173, #14762, #18346 ) ;
#20623=VECTOR ( 'NONE', #15037, 1000.000000000000227 ) ;
#20626=CARTESIAN_POINT ( 'NONE',  ( 117.1011158151309957, -12.73035498497280038, -19.59999999999999787 ) ) ;
#20629=CARTESIAN_POINT ( 'NONE',  ( 39.74442752440959481, 5.605205456207779768, -20.00000000000000000 ) ) ;
#20640=CONICAL_SURFACE ( 'NONE', #10425, 1.033499999999999863, 1.029744258676650093 ) ;
#20648=DIRECTION ( 'NONE',  ( -0.2306359803922076457, -0.9730401042858024541, 1.412237191019896446E-17 ) ) ;
#20654=CARTESIAN_POINT ( 'NONE',  ( 114.2412296582674429, -24.79605227811687485, -13.00000000000000000 ) ) ;
#20656=ADVANCED_FACE ( 'NONE', ( #6963 ), #21428, .T. ) ;
#20658=DIRECTION ( 'NONE',  ( -0.9730401042858024541, 0.2306359803922080898, 5.959266323858942451E-17 ) ) ;
#20681=DIRECTION ( 'NONE',  ( 0.2306359803922085339, 0.9730401042858022320, 0.000000000000000000 ) ) ;
#20685=CARTESIAN_POINT ( 'NONE',  ( 120.8697533057606961, 5.046729969097242474, 13.00000000000000000 ) ) ;
#20687=FACE_OUTER_BOUND ( 'NONE', #11016, .T. ) ;
#20691=ORIENTED_EDGE ( 'NONE', *, *, #3745, .T. ) ;
#20696=ORIENTED_EDGE ( 'NONE', *, *, #15419, .T. ) ;
#20699=CARTESIAN_POINT ( 'NONE',  ( 118.6002496876800052, -6.405594307115129560, 18.89999999999999858 ) ) ;
#20700=ADVANCED_FACE ( 'NONE', ( #19889 ), #1817, .T. ) ;
#20703=PLANE ( 'NONE',  #386 ) ;
#20706=AXIS2_PLACEMENT_3D ( 'NONE', #20050, #14706, #12595 ) ;
#20709=CARTESIAN_POINT ( 'NONE',  ( 113.4570673249340018, -28.10438863268850085, -3.399999999999949729 ) ) ;
#20712=EDGE_CURVE ( 'NONE', #21153, #2245, #9431, .T. ) ;
#20718=DIRECTION ( 'NONE',  ( -0.2306359803922081175, -0.9730401042858022320, 1.412237191019896138E-17 ) ) ;
#20741=UNCERTAINTY_MEASURE_WITH_UNIT (LENGTH_MEASURE( 1.000000000000000082E-05 ), #1653, 'distance_accuracy_value', 'NONE');
#20748=ORIENTED_EDGE ( 'NONE', *, *, #19611, .F. ) ;
#20749=ADVANCED_FACE ( 'NONE', ( #12867 ), #20109, .F. ) ;
#20759=AXIS2_PLACEMENT_3D ( 'NONE', #18117, #3848, #19661 ) ;
#20763=ORIENTED_EDGE ( 'NONE', *, *, #11595, .T. ) ;
#20777=DIRECTION ( 'NONE',  ( -1.164423685541379998E-14, -4.938475812832819565E-14, 1.000000000000000000 ) ) ;
#20781=ORIENTED_EDGE ( 'NONE', *, *, #13415, .F. ) ;
#20793=ORIENTED_EDGE ( 'NONE', *, *, #10155, .F. ) ;
#20794=CARTESIAN_POINT ( 'NONE',  ( 118.4388045014059969, -7.086722380115130449, 19.59999999999999787 ) ) ;
#20797=ADVANCED_FACE ( 'NONE', ( #10768 ), #8963, .T. ) ;
#20798=EDGE_CURVE ( 'NONE', #13304, #2609, #9791, .T. ) ;
#20802=CARTESIAN_POINT ( 'NONE',  ( 43.45766680872420551, 21.27115113520920175, -13.00000000000000000 ) ) ;
#20809=ORIENTED_EDGE ( 'NONE', *, *, #400, .T. ) ;
#20811=DIRECTION ( 'NONE',  ( 0.2306359803922080620, 0.9730401042858023430, -2.572202231434326974E-16 ) ) ;
#20818=CIRCLE ( 'NONE', #21623, 7.000000000000000888 ) ;
#20839=ORIENTED_EDGE ( 'NONE', *, *, #14908, .F. ) ;
#20840=FACE_OUTER_BOUND ( 'NONE', #11026, .T. ) ;
#20842=CARTESIAN_POINT ( 'NONE',  ( 117.0319250210129951, -13.02226701625859917, 18.89999999999999858 ) ) ;
#20843=ADVANCED_FACE ( 'NONE', ( #2290 ), #22583, .F. ) ;
#20852=CYLINDRICAL_SURFACE ( 'NONE', #6358, 2.066999999999998394 ) ;
#20854=EDGE_CURVE ( 'NONE', #104, #3196, #8128, .T. ) ;
#20856=ORIENTED_EDGE ( 'NONE', *, *, #9417, .F. ) ;
#20865=ORIENTED_EDGE ( 'NONE', *, *, #11412, .T. ) ;
#20874=VECTOR ( 'NONE', #1308, 1000.000000000000227 ) ;
#20887=CARTESIAN_POINT ( 'NONE',  ( 103.2898377416287303, 9.213630226843337212, 13.00000000000000000 ) ) ;
#20892=DIRECTION ( 'NONE',  ( -0.9730401042858024541, 0.2306359803922080898, 5.959266323858942451E-17 ) ) ;
#20906=FACE_OUTER_BOUND ( 'NONE', #5479, .T. ) ;
#20917=AXIS2_PLACEMENT_3D ( 'NONE', #19691, #23116, #5440 ) ;
#20931=DIRECTION ( 'NONE',  ( 0.9730401042858024541, -0.2306359803922080898, -5.959266323858942451E-17 ) ) ;
#20934=LINE ( 'NONE', #15477, #13597 ) ;
#20940=CARTESIAN_POINT ( 'NONE',  ( 113.2033677465029911, -29.17473274740290279, -3.099999999999920153 ) ) ;
#20947=ORIENTED_EDGE ( 'NONE', *, *, #15091, .T. ) ;
#20948=EDGE_CURVE ( 'NONE', #12703, #13133, #10395, .T. ) ;
#20952=LINE ( 'NONE', #640, #19317 ) ;
#20953=ORIENTED_EDGE ( 'NONE', *, *, #1385, .T. ) ;
#20954=CIRCLE ( 'NONE', #20199, 2.066999999999997950 ) ;
#20964=ADVANCED_FACE ( 'NONE', ( #15237 ), #6204, .F. ) ;
#20965=ADVANCED_FACE ( 'NONE', ( #10042, #9553, #13466 ), #16779, .T. ) ;
#20972=CARTESIAN_POINT ( 'NONE',  ( 118.6002496876800052, -6.405594307115070052, -15.90000000000000036 ) ) ;
#20976=ORIENTED_EDGE ( 'NONE', *, *, #8508, .T. ) ;
#20977=CARTESIAN_POINT ( 'NONE',  ( 105.8171986446039909, -20.23006919877430221, 13.00000000000000000 ) ) ;
#20979=AXIS2_PLACEMENT_3D ( 'NONE', #4432, #9682, #11352 ) ;
#20980=DIRECTION ( 'NONE',  ( -0.2306359803922080620, -0.9730401042858023430, -2.367063548676051037E-14 ) ) ;
#20984=ADVANCED_FACE ( 'NONE', ( #17267 ), #8233, .T. ) ;
#20987=ORIENTED_EDGE ( 'NONE', *, *, #1650, .F. ) ;
#20988=AXIS2_PLACEMENT_3D ( 'NONE', #20594, #16541, #9561 ) ;
#20995=ORIENTED_EDGE ( 'NONE', *, *, #13206, .F. ) ;
#21010=CIRCLE ( 'NONE', #22130, 2.066999999999997506 ) ;
#21024=EDGE_LOOP ( 'NONE', ( #21209, #20102, #2703, #10380 ) ) ;
#21025=ORIENTED_EDGE ( 'NONE', *, *, #17901, .F. ) ;
#21038=VERTEX_POINT ( 'NONE', #1203 ) ;
#21039=DIRECTION ( 'NONE',  ( 0.000000000000000000, -2.098117411679737831E-16, -1.000000000000000000 ) ) ;
#21041=CARTESIAN_POINT ( 'NONE',  ( 112.5523895830310011, 2.765522746992189251, -1.033499999999968111 ) ) ;
#21042=ORIENTED_EDGE ( 'NONE', *, *, #12843, .T. ) ;
#21047=VERTEX_POINT ( 'NONE', #21404 ) ;
#21048=DIRECTION ( 'NONE',  ( 0.000000000000000000, 0.000000000000000000, 1.000000000000000000 ) ) ;
#21056=DIRECTION ( 'NONE',  ( 0.2306359803922085339, 0.9730401042858022320, 0.000000000000000000 ) ) ;
#21057=AXIS2_PLACEMENT_3D ( 'NONE', #15717, #14825, #9743 ) ;
#21068=ORIENTED_EDGE ( 'NONE', *, *, #14363, .F. ) ;
#21074=AXIS2_PLACEMENT_3D ( 'NONE', #18233, #12542, #3509 ) ;
#21078=DIRECTION ( 'NONE',  ( -1.302733484953870109E-15, -5.237774525740650345E-15, -1.000000000000000000 ) ) ;
#21082=EDGE_CURVE ( 'NONE', #14758, #13082, #6441, .T. ) ;
#21087=AXIS2_PLACEMENT_3D ( 'NONE', #22917, #15799, #23265 ) ;
#21108=CARTESIAN_POINT ( 'NONE',  ( 117.1011158151309957, -12.73035498497280038, -20.00000000000000000 ) ) ;
#21109=VERTEX_POINT ( 'NONE', #1083 ) ;
#21111=VECTOR ( 'NONE', #4573, 1000.000000000000227 ) ;
#21114=ORIENTED_EDGE ( 'NONE', *, *, #19681, .F. ) ;
#21116=CARTESIAN_POINT ( 'NONE',  ( 37.67179450110460692, -4.077824265976569329, 13.00000000000000000 ) ) ;
#21118=EDGE_CURVE ( 'NONE', #9648, #2588, #9626, .T. ) ;
#21124=VERTEX_POINT ( 'NONE', #1442 ) ;
#21125=CARTESIAN_POINT ( 'NONE',  ( 113.4570673249340018, -28.10438863268850085, -2.700000000000000178 ) ) ;
#21128=EDGE_LOOP ( 'NONE', ( #5912, #11753, #11700, #336 ) ) ;
#21131=AXIS2_PLACEMENT_3D ( 'NONE', #6949, #19289, #13831 ) ;
#21135=EDGE_CURVE ( 'NONE', #14881, #12312, #8705, .T. ) ;
#21145=ADVANCED_FACE ( 'NONE', ( #15825 ), #17380, .T. ) ;
#21147=VECTOR ( 'NONE', #15976, 1000.000000000000114 ) ;
#21148=CIRCLE ( 'NONE', #18128, 2.066999999999999726 ) ;
#21151=AXIS2_PLACEMENT_3D ( 'NONE', #19897, #16434, #23208 ) ;
#21153=VERTEX_POINT ( 'NONE', #8940 ) ;
#21156=EDGE_LOOP ( 'NONE', ( #17285, #13538, #9422, #1152 ) ) ;
#21158=DIRECTION ( 'NONE',  ( -0.9730401042858022320, 0.2306359803922080343, 5.959266323858941219E-17 ) ) ;
#21159=DIRECTION ( 'NONE',  ( 0.9730401042858024541, -0.2306359803922080898, -5.959266323862942222E-17 ) ) ;
#21161=VECTOR ( 'NONE', #5297, 1000.000000000000227 ) ;
#21169=CARTESIAN_POINT ( 'NONE',  ( 118.6002496876800052, -6.405594307115070052, -15.90000000000000036 ) ) ;
#21187=VERTEX_POINT ( 'NONE', #232 ) ;
#21198=EDGE_LOOP ( 'NONE', ( #940, #1923, #12583, #15447 ) ) ;
#21209=ORIENTED_EDGE ( 'NONE', *, *, #2595, .T. ) ;
#21212=DIRECTION ( 'NONE',  ( 0.2306359803922080898, 0.9730401042858024541, -2.572202231434325988E-16 ) ) ;
#21224=ORIENTED_EDGE ( 'NONE', *, *, #22135, .F. ) ;
#21239=ADVANCED_FACE ( 'NONE', ( #1788 ), #7832, .F. ) ;
#21250=EDGE_CURVE ( 'NONE', #15573, #19560, #610, .T. ) ;
#21262=CARTESIAN_POINT ( 'NONE',  ( 114.6071564266699880, -22.31351932764730250, -13.00000000000000000 ) ) ;
#21268=ORIENTED_EDGE ( 'NONE', *, *, #8696, .F. ) ;
#21273=DIRECTION ( 'NONE',  ( -0.9730401042858024541, 0.2306359803922080898, 5.959266323858942451E-17 ) ) ;
#21285=EDGE_CURVE ( 'NONE', #5959, #19953, #3591, .T. ) ;
#21296=LINE ( 'NONE', #22838, #999 ) ;
#21301=EDGE_CURVE ( 'NONE', #11739, #6720, #10853, .T. ) ;
#21307=EDGE_CURVE ( 'NONE', #15573, #18769, #18075, .T. ) ;
#21310=LINE ( 'NONE', #14544, #18212 ) ;
#21312=VECTOR ( 'NONE', #5792, 1000.000000000000000 ) ;
#21321=AXIS2_PLACEMENT_3D ( 'NONE', #16396, #11076, #5359 ) ;
#21328=ORIENTED_EDGE ( 'NONE', *, *, #12555, .T. ) ;
#21336=CYLINDRICAL_SURFACE ( 'NONE', #14929, 0.3999999999999982458 ) ;
#21358=FACE_OUTER_BOUND ( 'NONE', #86, .T. ) ;
#21361=VECTOR ( 'NONE', #23244, 1000.000000000000000 ) ;
#21366=ORIENTED_EDGE ( 'NONE', *, *, #11009, .F. ) ;
#21368=EDGE_LOOP ( 'NONE', ( #20308, #10282, #19688, #2554 ) ) ;
#21369=AXIS2_PLACEMENT_3D ( 'NONE', #13923, #8701, #15929 ) ;
#21373=ORIENTED_EDGE ( 'NONE', *, *, #1696, .T. ) ;
#21388=FACE_OUTER_BOUND ( 'NONE', #7492, .T. ) ;
#21400=DIRECTION ( 'NONE',  ( -0.9730401042858022320, 0.2306359803922080343, 5.959266323858941219E-17 ) ) ;
#21404=CARTESIAN_POINT ( 'NONE',  ( 39.83668191656649782, 5.994421497922120423, -19.59999999999999787 ) ) ;
#21428=PLANE ( 'NONE',  #21713 ) ;
#21448=ADVANCED_FACE ( 'NONE', ( #13205 ), #20439, .T. ) ;
#21452=VERTEX_POINT ( 'NONE', #6063 ) ;
#21455=LINE ( 'NONE', #22884, #17146 ) ;
#21462=DIRECTION ( 'NONE',  ( 0.000000000000000000, -1.000000000000000000, 2.880774829024070580E-15 ) ) ;
#21464=ORIENTED_EDGE ( 'NONE', *, *, #12261, .T. ) ;
#21469=ADVANCED_FACE ( 'NONE', ( #20284 ), #18269, .F. ) ;
#21485=FACE_BOUND ( 'NONE', #17749, .T. ) ;
#21489=DIRECTION ( 'NONE',  ( -0.9730401042858024541, 0.2306359803922080898, 5.959266323858942451E-17 ) ) ;
#21500=EDGE_LOOP ( 'NONE', ( #11556, #7199, #14457 ) ) ;
#21503=DIRECTION ( 'NONE',  ( -0.2306359803922066187, -0.9730401042858026761, 0.000000000000000000 ) ) ;
#21505=DIRECTION ( 'NONE',  ( 0.2306359803922085339, 0.9730401042858022320, 0.000000000000000000 ) ) ;
#21509=CARTESIAN_POINT ( 'NONE',  ( 41.15130700480209924, 11.54075009235119964, -15.50000000000000000 ) ) ;
#21513=AXIS2_PLACEMENT_3D ( 'NONE', #1950, #8874, #14205 ) ;
#21514=CARTESIAN_POINT ( 'NONE',  ( 102.2474456857739966, -6.023754975411469204, 3.510479034365399954E-14 ) ) ;
#21516=CARTESIAN_POINT ( 'NONE',  ( 41.08211621068439712, 11.24883806106539907, 18.89999999999999858 ) ) ;
#21522=AXIS2_PLACEMENT_3D ( 'NONE', #15877, #14098, #5189 ) ;
#21532=DIRECTION ( 'NONE',  ( -2.471194949999149731E-15, -1.016744709403700171E-14, -1.000000000000000000 ) ) ;
#21535=CYLINDRICAL_SURFACE ( 'NONE', #5960, 0.4000000000000001887 ) ;
#21538=EDGE_CURVE ( 'NONE', #21933, #8196, #19809, .T. ) ;
#21543=DIRECTION ( 'NONE',  ( 0.2306359803922080898, 0.9730401042858024541, -2.572202231434325988E-16 ) ) ;
#21550=VERTEX_POINT ( 'NONE', #18150 ) ;
#21559=VERTEX_POINT ( 'NONE', #21813 ) ;
#21560=CARTESIAN_POINT ( 'NONE',  ( 118.5079952955230027, -6.794810348829359192, -15.50000000000000000 ) ) ;
#21579=DIRECTION ( 'NONE',  ( -0.9730401042858022320, 0.2306359803922080343, 5.959266323858941219E-17 ) ) ;
#21586=ORIENTED_EDGE ( 'NONE', *, *, #2389, .F. ) ;
#21593=EDGE_CURVE ( 'NONE', #19234, #19111, #16241, .T. ) ;
#21597=AXIS2_PLACEMENT_3D ( 'NONE', #889, #8152, #22728 ) ;
#21598=( GEOMETRIC_REPRESENTATION_CONTEXT ( 3 ) GLOBAL_UNCERTAINTY_ASSIGNED_CONTEXT ( ( #20741 ) ) GLOBAL_UNIT_ASSIGNED_CONTEXT ( ( #1653, #19595, #12481 ) ) REPRESENTATION_CONTEXT ( 'NONE', 'WORKASPACE' ) );
#21600=VECTOR ( 'NONE', #4038, 1000.000000000000227 ) ;
#21605=DIRECTION ( 'NONE',  ( -0.9730401042858022320, 0.2306359803922080343, 5.959266323858941219E-17 ) ) ;
#21607=ORIENTED_EDGE ( 'NONE', *, *, #4879, .F. ) ;
#21612=ORIENTED_EDGE ( 'NONE', *, *, #3745, .F. ) ;
#21614=DIRECTION ( 'NONE',  ( -5.204170427930418759E-14, -1.951563910473906971E-13, -1.000000000000000000 ) ) ;
#21623=AXIS2_PLACEMENT_3D ( 'NONE', #12891, #14669, #9452 ) ;
#21629=DIRECTION ( 'NONE',  ( -0.9730401042858022320, 0.2306359803922080343, 5.959266323858941219E-17 ) ) ;
#21644=EDGE_LOOP ( 'NONE', ( #23144, #9382, #12990, #19713 ) ) ;
#21657=DIRECTION ( 'NONE',  ( 0.000000000000000000, 0.000000000000000000, -1.000000000000000000 ) ) ;
#21663=DIRECTION ( 'NONE',  ( 0.1982893547227720377, 0.8365715274351381847, 0.5107146084541409614 ) ) ;
#21665=ORIENTED_EDGE ( 'NONE', *, *, #11082, .T. ) ;
#21670=AXIS2_PLACEMENT_3D ( 'NONE', #12576, #7010, #12462 ) ;
#21691=DIRECTION ( 'NONE',  ( 2.920245690604589998E-14, 1.234618914536939803E-13, -1.000000000000000000 ) ) ;
#21692=PLANE ( 'NONE',  #10321 ) ;
#21712=CIRCLE ( 'NONE', #22851, 2.066999999999997950 ) ;
#21713=AXIS2_PLACEMENT_3D ( 'NONE', #3369, #17867, #10640 ) ;
#21726=VERTEX_POINT ( 'NONE', #2340 ) ;
#21730=AXIS2_PLACEMENT_3D ( 'NONE', #1078, #15579, #21048 ) ;
#21734=DIRECTION ( 'NONE',  ( 0.2306359803922080343, 0.9730401042858022320, -2.539064864905560527E-14 ) ) ;
#21743=VERTEX_POINT ( 'NONE', #15393 ) ;
#21745=AXIS2_PLACEMENT_3D ( 'NONE', #9436, #16654, #4335 ) ;
#21746=CARTESIAN_POINT ( 'NONE',  ( 39.83668191656649782, 5.994421497922090225, -18.89999999999999858 ) ) ;
#21756=EDGE_LOOP ( 'NONE', ( #2984, #18942, #7353, #13392 ) ) ;
#21762=EDGE_CURVE ( 'NONE', #19270, #15831, #5187, .T. ) ;
#21765=EDGE_CURVE ( 'NONE', #21109, #2277, #6020, .T. ) ;
#21767=VERTEX_POINT ( 'NONE', #11634 ) ;
#21795=EDGE_LOOP ( 'NONE', ( #12015, #10581 ) ) ;
#21800=DIRECTION ( 'NONE',  ( -0.2306359803922087282, -0.9730401042858021210, 5.204170427930421283E-15 ) ) ;
#21802=ADVANCED_FACE ( 'NONE', ( #22278 ), #22164, .T. ) ;
#21803=EDGE_CURVE ( 'NONE', #13888, #14120, #2582, .T. ) ;
#21805=CARTESIAN_POINT ( 'NONE',  ( 45.07211867146970263, 28.08243186520990164, 13.00000000000000000 ) ) ;
#21807=CIRCLE ( 'NONE', #10473, 2.499999999999999112 ) ;
#21810=DIRECTION ( 'NONE',  ( -0.9730401042858022320, 0.2306359803922080343, 5.959266323858941219E-17 ) ) ;
#21813=CARTESIAN_POINT ( 'NONE',  ( 115.3944095602285387, -19.93085175668762332, 13.00000000000000000 ) ) ;
#21826=VECTOR ( 'NONE', #16100, 1000.000000000000227 ) ;
#21839=CARTESIAN_POINT ( 'NONE',  ( 118.4388045014059969, -7.086722380115130449, 19.59999999999999787 ) ) ;
#21856=VECTOR ( 'NONE', #7397, 1000.000000000000000 ) ;
#21858=CIRCLE ( 'NONE', #15412, 2.499999999999998224 ) ;
#21870=CARTESIAN_POINT ( 'NONE',  ( 39.76749112244880280, 5.702509466636339397, 15.50000000000000000 ) ) ;
#21872=DIRECTION ( 'NONE',  ( 6.124378941434239724E-17, -2.274246353359159970E-33, 1.000000000000000000 ) ) ;
#21882=ORIENTED_EDGE ( 'NONE', *, *, #4735, .F. ) ;
#21898=CARTESIAN_POINT ( 'NONE',  ( 36.10037903421270755, -9.768828191507928693, -2.700000000000000178 ) ) ;
#21905=AXIS2_PLACEMENT_3D ( 'NONE', #14425, #21543, #21657 ) ;
#21933=VERTEX_POINT ( 'NONE', #17773 ) ;
#21938=CARTESIAN_POINT ( 'NONE',  ( 114.9405074087380001, 12.84085624101770051, 2.915350241847199977E-14 ) ) ;
#21942=DIRECTION ( 'NONE',  ( -0.2306359803922080343, -0.9730401042858022320, -7.611545645951921999E-14 ) ) ;
#21974=ORIENTED_EDGE ( 'NONE', *, *, #18961, .T. ) ;
#21975=VECTOR ( 'NONE', #4689, 1000.000000000000227 ) ;
#21984=FACE_OUTER_BOUND ( 'NONE', #15869, .T. ) ;
#22003=VECTOR ( 'NONE', #19510, 1000.000000000000114 ) ;
#22005=FACE_OUTER_BOUND ( 'NONE', #21024, .T. ) ;
#22015=LINE ( 'NONE', #14664, #17975 ) ;
#22017=AXIS2_PLACEMENT_3D ( 'NONE', #7031, #21489, #8920 ) ;
#22026=ORIENTED_EDGE ( 'NONE', *, *, #21593, .F. ) ;
#22034=ORIENTED_EDGE ( 'NONE', *, *, #22160, .T. ) ;
#22040=ORIENTED_EDGE ( 'NONE', *, *, #9478, .F. ) ;
#22042=CARTESIAN_POINT ( 'NONE',  ( 114.8905747189831033, 12.63019305843987361, -2.067000000000024595 ) ) ;
#22045=AXIS2_PLACEMENT_3D ( 'NONE', #10497, #21273, #21505 ) ;
#22055=DIRECTION ( 'NONE',  ( 0.000000000000000000, 0.000000000000000000, -1.000000000000000000 ) ) ;
#22058=CARTESIAN_POINT ( 'NONE',  ( 122.7747609327790030, 11.20643158045800014, 9.133960000000000079 ) ) ;
#22064=CONICAL_SURFACE ( 'NONE', #7306, 2.283500000000000085, 0.7853981633974447263 ) ;
#22081=ORIENTED_EDGE ( 'NONE', *, *, #15006, .F. ) ;
#22094=EDGE_CURVE ( 'NONE', #20342, #15812, #22611, .T. ) ;
#22098=AXIS2_PLACEMENT_3D ( 'NONE', #14352, #12361, #19581 ) ;
#22109=CARTESIAN_POINT ( 'NONE',  ( 36.79228697538940196, -6.849707878650439952, 3.399999999999999911 ) ) ;
#22123=DIRECTION ( 'NONE',  ( 0.5249589903860194529, -0.8511275218278935295, 5.444325428271645316E-17 ) ) ;
#22124=FACE_OUTER_BOUND ( 'NONE', #11696, .T. ) ;
#22130=AXIS2_PLACEMENT_3D ( 'NONE', #4708, #6845, #17302 ) ;
#22134=ADVANCED_FACE ( 'NONE', ( #13956 ), #4049, .F. ) ;
#22135=EDGE_CURVE ( 'NONE', #10848, #23125, #15500, .T. ) ;
#22139=EDGE_CURVE ( 'NONE', #19161, #16449, #22730, .T. ) ;
#22142=ORIENTED_EDGE ( 'NONE', *, *, #2595, .F. ) ;
#22146=DIRECTION ( 'NONE',  ( 0.9730401042858024541, -0.2306359803922080898, -5.959266323858942451E-17 ) ) ;
#22152=ADVANCED_FACE ( 'NONE', ( #9820 ), #20355, .F. ) ;
#22155=DIRECTION ( 'NONE',  ( 0.9730401042858024541, -0.2306359803922080898, -5.959266323858942451E-17 ) ) ;
#22160=EDGE_CURVE ( 'NONE', #3328, #1999, #23373, .T. ) ;
#22164=PLANE ( 'NONE',  #16560 ) ;
#22186=EDGE_CURVE ( 'NONE', #22407, #10583, #19191, .T. ) ;
#22189=FACE_OUTER_BOUND ( 'NONE', #1165, .T. ) ;
#22196=ORIENTED_EDGE ( 'NONE', *, *, #21803, .T. ) ;
#22197=VERTEX_POINT ( 'NONE', #4810 ) ;
#22203=CARTESIAN_POINT ( 'NONE',  ( 117.1933702072879981, -12.34113894325849969, -18.89999999999999858 ) ) ;
#22204=LINE ( 'NONE', #6638, #4851 ) ;
#22227=AXIS2_PLACEMENT_3D ( 'NONE', #19521, #2898, #4912 ) ;
#22234=EDGE_CURVE ( 'NONE', #3328, #14157, #8969, .T. ) ;
#22238=VECTOR ( 'NONE', #22392, 1000.000000000000227 ) ;
#22253=VERTEX_POINT ( 'NONE', #1822 ) ;
#22259=AXIS2_PLACEMENT_3D ( 'NONE', #3947, #18329, #20681 ) ;
#22270=LINE ( 'NONE', #20629, #19866 ) ;
#22278=FACE_OUTER_BOUND ( 'NONE', #18686, .T. ) ;
#22300=LINE ( 'NONE', #6040, #3157 ) ;
#22301=EDGE_LOOP ( 'NONE', ( #17004, #21665, #3607, #11770 ) ) ;
#22307=DIRECTION ( 'NONE',  ( 0.9730401042858024541, -0.2306359803922080898, -5.959266323858942451E-17 ) ) ;
#22322=DIRECTION ( 'NONE',  ( -0.9730401042858022320, 0.2306359803922080343, -2.396759184561635323E-31 ) ) ;
#22333=ORIENTED_EDGE ( 'NONE', *, *, #4516, .F. ) ;
#22340=ORIENTED_EDGE ( 'NONE', *, *, #16315, .T. ) ;
#22343=DIRECTION ( 'NONE',  ( 0.9730401042858024541, -0.2306359803922080898, -5.959266323858942451E-17 ) ) ;
#22366=DIRECTION ( 'NONE',  ( -0.9730401042858024541, 0.2306359803922080898, 5.959266323859212389E-17 ) ) ;
#22376=CARTESIAN_POINT ( 'NONE',  ( 43.45766680872420551, 21.27115113520920175, -13.00000000000000000 ) ) ;
#22385=EDGE_CURVE ( 'NONE', #10964, #990, #2562, .T. ) ;
#22392=DIRECTION ( 'NONE',  ( -0.2306359803922080343, -0.9730401042858022320, 1.412237191019910313E-17 ) ) ;
#22395=ADVANCED_FACE ( 'NONE', ( #10773 ), #21535, .T. ) ;
#22401=CARTESIAN_POINT ( 'NONE',  ( 112.6956120935907251, 3.369770385951718517, -2.066999999999968196 ) ) ;
#22407=VERTEX_POINT ( 'NONE', #9685 ) ;
#22415=ADVANCED_FACE ( 'NONE', ( #9556 ), #14689, .F. ) ;
#22420=EDGE_LOOP ( 'NONE', ( #10883, #8043, #222, #19348 ) ) ;
#22428=ORIENTED_EDGE ( 'NONE', *, *, #15449, .F. ) ;
#22435=ORIENTED_EDGE ( 'NONE', *, *, #14769, .T. ) ;
#22441=ORIENTED_EDGE ( 'NONE', *, *, #3410, .T. ) ;
#22443=CARTESIAN_POINT ( 'NONE',  ( 117.1933702072879981, -12.34113894325840022, 18.89999999999999858 ) ) ;
#22460=ADVANCED_FACE ( 'NONE', ( #16900 ), #11237, .F. ) ;
#22464=CARTESIAN_POINT ( 'NONE',  ( 61.93563330948219203, 19.01565939351215206, 13.00000000000000000 ) ) ;
#22466=CARTESIAN_POINT ( 'NONE',  ( 117.0319250210129951, -13.02226701625849969, -18.89999999999999858 ) ) ;
#22476=CARTESIAN_POINT ( 'NONE',  ( 114.6071564266699880, -22.31351932764730250, 13.00000000000000000 ) ) ;
#22492=CARTESIAN_POINT ( 'NONE',  ( 35.93893384793820189, -10.44995626450799975, -2.700000000000000178 ) ) ;
#22493=AXIS2_PLACEMENT_3D ( 'NONE', #4267, #17325, #18648 ) ;
#22494=ADVANCED_FACE ( 'NONE', ( #22124 ), #155, .T. ) ;
#22501=ORIENTED_EDGE ( 'NONE', *, *, #13891, .T. ) ;
#22523=ORIENTED_EDGE ( 'NONE', *, *, #6305, .T. ) ;
#22537=DIRECTION ( 'NONE',  ( -0.2306359803922094498, -0.9730401042858020100, 1.412237191019847142E-17 ) ) ;
#22551=ORIENTED_EDGE ( 'NONE', *, *, #8477, .F. ) ;
#22556=EDGE_LOOP ( 'NONE', ( #3791, #7757 ) ) ;
#22563=EDGE_CURVE ( 'NONE', #563, #18262, #19051, .T. ) ;
#22573=FACE_BOUND ( 'NONE', #17635, .T. ) ;
#22583=CYLINDRICAL_SURFACE ( 'NONE', #20979, 2.066999999999999726 ) ;
#22587=DIRECTION ( 'NONE',  ( -0.2306359803922080898, -0.9730401042858024541, 2.572202231434325988E-16 ) ) ;
#22589=EDGE_CURVE ( 'NONE', #18063, #21559, #646, .T. ) ;
#22598=DIRECTION ( 'NONE',  ( 0.2306359803921919083, 0.9730401042858062288, 1.301042606982611127E-13 ) ) ;
#22607=ORIENTED_EDGE ( 'NONE', *, *, #1857, .T. ) ;
#22611=LINE ( 'NONE', #9944, #1759 ) ;
#22612=ADVANCED_FACE ( 'NONE', ( #13471 ), #13823, .T. ) ;
#22613=AXIS2_PLACEMENT_3D ( 'NONE', #7051, #10738, #10969 ) ;
#22619=CARTESIAN_POINT ( 'NONE',  ( 117.0319250210129951, -13.02226701625859917, 18.89999999999999858 ) ) ;
#22623=CARTESIAN_POINT ( 'NONE',  ( 120.3930287342899987, 3.035456073538439714, -13.00000000000000000 ) ) ;
#22639=VECTOR ( 'NONE', #22123, 1000.000000000000000 ) ;
#22648=AXIS2_PLACEMENT_3D ( 'NONE', #15340, #19028, #4414 ) ;
#22654=AXIS2_PLACEMENT_3D ( 'NONE', #11147, #15024, #9458 ) ;
#22671=VECTOR ( 'NONE', #4584, 1000.000000000000000 ) ;
#22676=EDGE_CURVE ( 'NONE', #12333, #19198, #4844, .T. ) ;
#22685=FACE_OUTER_BOUND ( 'NONE', #7603, .T. ) ;
#22689=EDGE_CURVE ( 'NONE', #19560, #15573, #21148, .T. ) ;
#22703=AXIS2_PLACEMENT_3D ( 'NONE', #6001, #885, #8148 ) ;
#22722=PLANE ( 'NONE',  #22703 ) ;
#22725=VECTOR ( 'NONE', #1814, 1000.000000000000000 ) ;
#22728=DIRECTION ( 'NONE',  ( 6.124378941434239724E-17, -2.274246353359159970E-33, 1.000000000000000000 ) ) ;
#22730=LINE ( 'NONE', #20842, #21111 ) ;
#22736=CONICAL_SURFACE ( 'NONE', #6066, 2.283500000000000529, 0.7853981633974469467 ) ;
#22747=DIRECTION ( 'NONE',  ( -0.9730401042858022320, 0.2306359803922080343, 5.959266323858941219E-17 ) ) ;
#22751=ADVANCED_FACE ( 'NONE', ( #12820 ), #12710, .F. ) ;
#22752=LINE ( 'NONE', #13745, #6538 ) ;
#22777=CARTESIAN_POINT ( 'NONE',  ( 61.45890873801150178, 17.00438549795339682, 13.00000000000000000 ) ) ;
#22781=EDGE_LOOP ( 'NONE', ( #14292, #10474, #19545, #17369, #15137, #14237, #1474, #22333, #10010, #7996, #17364, #1350, #9093, #8657, #20066, #19556, #1368, #14535, #17162, #17404, #13644, #15144, #424, #21025, #14819, #14698, #2756, #147, #18149, #12751, #11046, #5308, #23470, #18446, #14259, #8463, #12779, #16997, #12247, #20153, #3192, #13310, #14983, #14959, #22551, #11581, #22959, #18846 ) ) ;
#22791=ADVANCED_FACE ( 'NONE', ( #3564 ), #12597, .T. ) ;
#22810=DIRECTION ( 'NONE',  ( 3.469446951953605354E-14, 9.757819552369514663E-14, -1.000000000000000000 ) ) ;
#22825=CARTESIAN_POINT ( 'NONE',  ( 114.8178196092480050, -22.36345201740219935, 13.00000000000000000 ) ) ;
#22836=CARTESIAN_POINT ( 'NONE',  ( 120.0770346556423931, 0.7635863056469011090, -13.00000000000000000 ) ) ;
#22837=AXIS2_PLACEMENT_3D ( 'NONE', #20802, #10378, #4531 ) ;
#22838=CARTESIAN_POINT ( 'NONE',  ( 118.4388045014059969, -7.086722380115170417, -18.89999999999999858 ) ) ;
#22842=ORIENTED_EDGE ( 'NONE', *, *, #8270, .F. ) ;
#22849=ORIENTED_EDGE ( 'NONE', *, *, #18961, .F. ) ;
#22850=VECTOR ( 'NONE', #14495, 1000.000000000000000 ) ;
#22851=AXIS2_PLACEMENT_3D ( 'NONE', #15018, #9706, #884 ) ;
#22865=EDGE_CURVE ( 'NONE', #9929, #22253, #9027, .T. ) ;
#22877=CARTESIAN_POINT ( 'NONE',  ( 114.8178196092480050, -22.36345201740219935, -13.00000000000000000 ) ) ;
#22884=CARTESIAN_POINT ( 'NONE',  ( 114.8178196092480050, -22.36345201740209987, 20.00000000000000000 ) ) ;
#22888=ORIENTED_EDGE ( 'NONE', *, *, #1657, .F. ) ;
#22901=VECTOR ( 'NONE', #18424, 1000.000000000000227 ) ;
#22902=DIRECTION ( 'NONE',  ( -0.9730401042858024541, 0.2306359803922080898, 5.959266323858862332E-17 ) ) ;
#22909=DIRECTION ( 'NONE',  ( -0.2306359803922080343, -0.9730401042858022320, -3.574477303645861237E-15 ) ) ;
#22912=EDGE_CURVE ( 'NONE', #2044, #18542, #20298, .T. ) ;
#22917=CARTESIAN_POINT ( 'NONE',  ( 96.81657767996070163, -18.09668638014640152, -13.00000000000000000 ) ) ;
#22919=EDGE_CURVE ( 'NONE', #18542, #2044, #11217, .T. ) ;
#22921=CARTESIAN_POINT ( 'NONE',  ( 45.07211867146960316, 28.08243186520980217, 10.02499999999999858 ) ) ;
#22927=ORIENTED_EDGE ( 'NONE', *, *, #22234, .T. ) ;
#22932=DIRECTION ( 'NONE',  ( -0.9730401042858024541, 0.2306359803922080898, 5.959266323858942451E-17 ) ) ;
#22939=CARTESIAN_POINT ( 'NONE',  ( 35.93893384793820189, -10.44995626450799975, -3.100000000000000089 ) ) ;
#22951=CARTESIAN_POINT ( 'NONE',  ( 102.8131131701580046, 7.202356331284469171, -13.00000000000000000 ) ) ;
#22952=EDGE_CURVE ( 'NONE', #990, #16449, #2598, .T. ) ;
#22953=CARTESIAN_POINT ( 'NONE',  ( 118.5310588935630136, -6.697506338400800452, -20.00000000000000000 ) ) ;
#22958=VERTEX_POINT ( 'NONE', #6155 ) ;
#22959=ORIENTED_EDGE ( 'NONE', *, *, #17179, .F. ) ;
#22974=ORIENTED_EDGE ( 'NONE', *, *, #12359, .F. ) ;
#22975=DIRECTION ( 'NONE',  ( -0.9730401042858024541, 0.2306359803922080898, 5.959266323858942451E-17 ) ) ;
#22986=ORIENTED_EDGE ( 'NONE', *, *, #14908, .T. ) ;
#22992=ORIENTED_EDGE ( 'NONE', *, *, #3160, .F. ) ;
#22999=CARTESIAN_POINT ( 'NONE',  ( 50.90756547144189881, 18.01515514085709668, 3.544128957608909560E-14 ) ) ;
#23001=EDGE_CURVE ( 'NONE', #17831, #17030, #6664, .T. ) ;
#23004=CIRCLE ( 'NONE', #20357, 0.4000000000000001887 ) ;
#23015=LINE ( 'NONE', #4980, #17824 ) ;
#23039=DIRECTION ( 'NONE',  ( -0.9730401042858024541, 0.2306359803922080898, 5.959266323863413074E-17 ) ) ;
#23040=DIRECTION ( 'NONE',  ( -0.5249589903860224505, 0.8511275218278915311, 1.187479569643817911E-16 ) ) ;
#23041=AXIS2_PLACEMENT_3D ( 'NONE', #18225, #1946, #19656 ) ;
#23048=ADVANCED_FACE ( 'NONE', ( #9371 ), #13413, .F. ) ;
#23049=ORIENTED_EDGE ( 'NONE', *, *, #2394, .T. ) ;
#23065=DIRECTION ( 'NONE',  ( -1.578894428126670167E-37, -2.578073951805180219E-21, 1.000000000000000000 ) ) ;
#23067=CARTESIAN_POINT ( 'NONE',  ( 117.0319250210129951, -13.02226701625849969, -15.90000000000000036 ) ) ;
#23080=EDGE_CURVE ( 'NONE', #3586, #8816, #13857, .T. ) ;
#23087=DIRECTION ( 'NONE',  ( 1.304396158928240120E-15, 5.761557392269829876E-15, -1.000000000000000000 ) ) ;
#23088=DIRECTION ( 'NONE',  ( -0.9730401042858024541, 0.2306359803922080898, 5.959266323858852472E-17 ) ) ;
#23094=ORIENTED_EDGE ( 'NONE', *, *, #14190, .F. ) ;
#23096=CARTESIAN_POINT ( 'NONE',  ( 59.43368109719860826, 4.124228161845699958, 3.772686752615189359E-14 ) ) ;
#23097=VERTEX_POINT ( 'NONE', #7710 ) ;
#23100=LINE ( 'NONE', #13981, #11864 ) ;
#23114=EDGE_CURVE ( 'NONE', #19111, #6605, #21807, .T. ) ;
#23116=DIRECTION ( 'NONE',  ( -0.9730401042858024541, 0.2306359803922080898, 5.959266323858942451E-17 ) ) ;
#23118=EDGE_LOOP ( 'NONE', ( #22196, #10556, #10730, #15841 ) ) ;
#23123=EDGE_LOOP ( 'NONE', ( #1454, #16557, #3173, #22040 ) ) ;
#23125=VERTEX_POINT ( 'NONE', #17213 ) ;
#23127=VERTEX_POINT ( 'NONE', #8179 ) ;
#23144=ORIENTED_EDGE ( 'NONE', *, *, #7453, .T. ) ;
#23149=CARTESIAN_POINT ( 'NONE',  ( 117.1933702072879981, -12.34113894325849969, -18.89999999999999858 ) ) ;
#23180=CONICAL_SURFACE ( 'NONE', #1568, 1.033499999999999863, 1.029744258676650093 ) ;
#23188=EDGE_LOOP ( 'NONE', ( #15578, #12140, #20107, #6145 ) ) ;
#23190=CARTESIAN_POINT ( 'NONE',  ( 53.10252809683450437, 27.27557781334509812, 3.299332471243299474E-14 ) ) ;
#23208=DIRECTION ( 'NONE',  ( 0.000000000000000000, 0.000000000000000000, -1.000000000000000000 ) ) ;
#23216=CARTESIAN_POINT ( 'NONE',  ( 102.2474456857739966, -6.023754975411469204, 3.510479034365399954E-14 ) ) ;
#23232=ORIENTED_EDGE ( 'NONE', *, *, #6641, .F. ) ;
#23234=AXIS2_PLACEMENT_3D ( 'NONE', #2479, #7939, #22055 ) ;
#23236=AXIS2_PLACEMENT_3D ( 'NONE', #10478, #12137, #15909 ) ;
#23244=DIRECTION ( 'NONE',  ( 0.5249589903860194529, -0.8511275218278935295, 5.444325428271645316E-17 ) ) ;
#23255=ORIENTED_EDGE ( 'NONE', *, *, #412, .F. ) ;
#23265=DIRECTION ( 'NONE',  ( -0.2306359803922053142, -0.9730401042858028982, 0.000000000000000000 ) ) ;
#23273=LINE ( 'NONE', #5789, #8377 ) ;
#23277=LINE ( 'NONE', #19603, #5599 ) ;
#23307=CARTESIAN_POINT ( 'NONE',  ( 114.8178196092480050, -22.36345201740219935, 13.00000000000000000 ) ) ;
#23311=ORIENTED_EDGE ( 'NONE', *, *, #21762, .T. ) ;
#23315=ADVANCED_FACE ( 'NONE', ( #19685 ), #179, .F. ) ;
#23326=DIRECTION ( 'NONE',  ( -0.2306359803922080343, -0.9730401042858022320, 1.412237191019910313E-17 ) ) ;
#23333=DIRECTION ( 'NONE',  ( 0.2306359803922080343, 0.9730401042858022320, -1.412237191019910313E-17 ) ) ;
#23342=FACE_OUTER_BOUND ( 'NONE', #23188, .T. ) ;
#23344=EDGE_CURVE ( 'NONE', #14253, #14262, #15772, .T. ) ;
#23345=CARTESIAN_POINT ( 'NONE',  ( 114.8178196092480050, -22.36345201740219935, 13.00000000000000000 ) ) ;
#23348=CARTESIAN_POINT ( 'NONE',  ( 52.45828777336780036, 19.13776831658130106, -13.00000000000000000 ) ) ;
#23354=CARTESIAN_POINT ( 'NONE',  ( 121.1303491780936099, 5.207460461920159212, -13.00000000000000000 ) ) ;
#23363=VERTEX_POINT ( 'NONE', #10566 ) ;
#23366=ORIENTED_EDGE ( 'NONE', *, *, #4262, .T. ) ;
#23373=CIRCLE ( 'NONE', #2541, 2.066999999999999726 ) ;
#23389=DIRECTION ( 'NONE',  ( 0.8511275218278948618, 0.5249589903860170104, -5.212440122911309516E-17 ) ) ;
#23390=ORIENTED_EDGE ( 'NONE', *, *, #20000, .F. ) ;
#23398=FACE_OUTER_BOUND ( 'NONE', #8146, .T. ) ;
#23401=DIRECTION ( 'NONE',  ( -5.791496838535410422E-15, -2.469238035320170149E-14, 1.000000000000000000 ) ) ;
#23408=AXIS2_PLACEMENT_3D ( 'NONE', #1475, #23087, #12094 ) ;
#23414=CARTESIAN_POINT ( 'NONE',  ( 117.1933702072879981, -12.34113894325849969, -18.89999999999999858 ) ) ;
#23418=DIRECTION ( 'NONE',  ( -0.9730401042858024541, 0.2306359803922080898, 5.959266323858952312E-17 ) ) ;
#23425=CARTESIAN_POINT ( 'NONE',  ( 116.5619150869516290, -6.333538388044982703, 3.459551998232740566E-14 ) ) ;
#23427=AXIS2_PLACEMENT_3D ( 'NONE', #20626, #20497, #9825 ) ;
#23429=DIRECTION ( 'NONE',  ( -0.9730401042858024541, 0.2306359803922080898, 5.959266323858942451E-17 ) ) ;
#23434=EDGE_CURVE ( 'NONE', #16110, #12330, #15371, .T. ) ;
#23458=VERTEX_POINT ( 'NONE', #21805 ) ;
#23464=LINE ( 'NONE', #10803, #3937 ) ;
#23470=ORIENTED_EDGE ( 'NONE', *, *, #19122, .F. ) ;
#23472=CARTESIAN_POINT ( 'NONE',  ( 113.8430260960419957, 8.210644904773758412, -2.066999999999969528 ) ) ;
#23515=COLOUR_RGB('Deep Blue', 0.09019608, 0.27058824, 0.51372549);
#23516=FILL_AREA_STYLE_COLOUR('',#23515);
#23517=FILL_AREA_STYLE('',(#23516));
#23518=SURFACE_STYLE_FILL_AREA(#23517);
#23519=SURFACE_SIDE_STYLE('',(#23518));
#23520=SURFACE_STYLE_USAGE(.BOTH.,#23519);
#23521=PRESENTATION_STYLE_ASSIGNMENT((#23520));
#23603=STYLED_ITEM('',(#23521),#9171);
#23604=MECHANICAL_DESIGN_GEOMETRIC_PRESENTATION_REPRESENTATION('',(#23603),#21598);
ENDSEC;
END-ISO-10303-21;
